ISO-10303-21;
HEADER;
FILE_DESCRIPTION (('STEP AP214'),
    '1' );
FILE_NAME ('Caster Wheel Tread.step',
    '2026-10-09T12:05:53',
    ( '' ),
    ( '' ),
    'SwSTEP 2.0',
    'SolidWorks 2026',
    '' );
FILE_SCHEMA (( 'AUTOMOTIVE_DESIGN' ));
ENDSEC;

DATA;
#25=CIRCLE ( 'NONE', #830, 16.00000000000000000 ) ;
#98=DIRECTION ( 'NONE',  ( 1.681650659181820092E-11, -1.000000000000000000, -2.220771714818679968E-11 ) ) ;
#99=ORIENTED_EDGE ( 'NONE', *, *, #38277, .T. ) ;
#102=CARTESIAN_POINT ( 'NONE',  ( 52.13393739769618662, -30.49118894467929763, -65.65000000000000568 ) ) ;
#171=DIRECTION ( 'NONE',  ( 8.402539340422011355E-12, -1.000000000000000000, -1.365304166073849981E-11 ) ) ;
#186=DIRECTION ( 'NONE',  ( 0.000000000000000000, 1.000000000000000000, 0.000000000000000000 ) ) ;
#202=CARTESIAN_POINT ( 'NONE',  ( 68.13393739769618662, -1.166188944679350081, -90.65000000000000568 ) ) ;
#238=DIRECTION ( 'NONE',  ( 0.000000000000000000, 1.000000000000000000, 0.000000000000000000 ) ) ;
#247=ORIENTED_EDGE ( 'NONE', *, *, #26711, .F. ) ;
#259=SHAPE_DEFINITION_REPRESENTATION ( #50860, #49550 ) ;
#286=DIRECTION ( 'NONE',  ( 1.000000000000000000, 0.000000000000000000, -1.224646799147353207E-16 ) ) ;
#291=EDGE_CURVE ( 'NONE', #43185, #32513, #25957, .T. ) ;
#389=EDGE_CURVE ( 'NONE', #27054, #15604, #37779, .T. ) ;
#407=DIRECTION ( 'NONE',  ( 0.5720614028176879140, -0.7071067811865481278, 0.4156269377774475249 ) ) ;
#413=ORIENTED_EDGE ( 'NONE', *, *, #32309, .F. ) ;
#421=CARTESIAN_POINT ( 'NONE',  ( 68.13393739806078031, -1.166188945131049870, -65.65000000072619457 ) ) ;
#484=ORIENTED_EDGE ( 'NONE', *, *, #27774, .F. ) ;
#503=CARTESIAN_POINT ( 'NONE',  ( 68.13393739806078031, -1.166188944679350081, -41.65000000083975351 ) ) ;
#511=ORIENTED_EDGE ( 'NONE', *, *, #15909, .F. ) ;
#617=EDGE_LOOP ( 'NONE', ( #818, #18947 ) ) ;
#746=CIRCLE ( 'NONE', #22514, 6.099999999999994316 ) ;
#770=DIRECTION ( 'NONE',  ( -1.000000000000000000, 0.000000000000000000, 0.000000000000000000 ) ) ;
#818=ORIENTED_EDGE ( 'NONE', *, *, #24467, .F. ) ;
#830=AXIS2_PLACEMENT_3D ( 'NONE', #20779, #32822, #5345 ) ;
#902=CIRCLE ( 'NONE', #46115, 16.50000000000000000 ) ;
#908=CIRCLE ( 'NONE', #9309, 25.00000000000000000 ) ;
#915=ORIENTED_EDGE ( 'NONE', *, *, #39393, .F. ) ;
#984=EDGE_CURVE ( 'NONE', #15604, #20784, #5928, .T. ) ;
#996=ORIENTED_EDGE ( 'NONE', *, *, #27776, .F. ) ;
#1014=CARTESIAN_POINT ( 'NONE',  ( 68.13393739769618662, -29.66618894467940137, -65.65000000000000568 ) ) ;
#1021=CARTESIAN_POINT ( 'NONE',  ( 68.13393739769618662, -28.80002732851770020, -29.09832030244573176 ) ) ;
#1043=FACE_OUTER_BOUND ( 'NONE', #5297, .T. ) ;
#1053=( NAMED_UNIT ( * ) PLANE_ANGLE_UNIT ( ) SI_UNIT ( $, .RADIAN. ) );
#1073=CYLINDRICAL_SURFACE ( 'NONE', #49651, 16.00000000000000000 ) ;
#1090=CIRCLE ( 'NONE', #16995, 23.50000000000000000 ) ;
#1215=EDGE_CURVE ( 'NONE', #43941, #37382, #5116, .T. ) ;
#1253=VECTOR ( 'NONE', #27515, 1000.000000000000114 ) ;
#1339=CARTESIAN_POINT ( 'NONE',  ( 68.13393739769618662, -1.166188944679350081, -40.64999999999999858 ) ) ;
#1421=AXIS2_PLACEMENT_3D ( 'NONE', #4906, #5181, #37141 ) ;
#1488=DIRECTION ( 'NONE',  ( -1.000000000000000000, -0.000000000000000000, -0.000000000000000000 ) ) ;
#1490=EDGE_CURVE ( 'NONE', #28355, #28663, #908, .T. ) ;
#1506=CIRCLE ( 'NONE', #35809, 7.599999999999996092 ) ;
#1527=VERTEX_POINT ( 'NONE', #42145 ) ;
#1557=CARTESIAN_POINT ( 'NONE',  ( 68.13393739769618662, -30.49118894467929763, -65.65000000000000568 ) ) ;
#1602=ORIENTED_EDGE ( 'NONE', *, *, #36920, .F. ) ;
#1759=ADVANCED_FACE ( 'NONE', ( #34130 ), #26032, .F. ) ;
#1765=DIRECTION ( 'NONE',  ( 0.000000000000000000, 1.000000000000000000, 0.000000000000000000 ) ) ;
#1822=CARTESIAN_POINT ( 'NONE',  ( 68.13393739769658453, -28.80002732851960445, -29.09832030244560741 ) ) ;
#1826=ADVANCED_FACE ( 'NONE', ( #11605 ), #6835, .T. ) ;
#1865=DIRECTION ( 'NONE',  ( 0.000000000000000000, 1.000000000000000000, 0.000000000000000000 ) ) ;
#1888=EDGE_CURVE ( 'NONE', #28919, #42024, #42043, .T. ) ;
#1899=CARTESIAN_POINT ( 'NONE',  ( 68.13393739769618662, -1.166188944679350081, -65.65000000000000568 ) ) ;
#1959=DIRECTION ( 'NONE',  ( 0.000000000000000000, 1.000000000000000000, 0.000000000000000000 ) ) ;
#1960=EDGE_CURVE ( 'NONE', #39247, #15377, #38368, .T. ) ;
#1970=CARTESIAN_POINT ( 'NONE',  ( 68.13393739769618662, -30.66618894467940137, -40.64999999999999858 ) ) ;
#1996=CARTESIAN_POINT ( 'NONE',  ( 68.13393739769618662, -29.66618894467940137, -65.65000000000000568 ) ) ;
#1997=ORIENTED_EDGE ( 'NONE', *, *, #26711, .T. ) ;
#2050=TOROIDAL_SURFACE ( 'NONE', #31315, 14.50000000000000000, 1.500000000000000000 ) ;
#2139=DIRECTION ( 'NONE',  ( -1.000000000000000000, 0.000000000000000000, 0.000000000000000000 ) ) ;
#2223=LINE ( 'NONE', #18200, #30963 ) ;
#2285=ORIENTED_EDGE ( 'NONE', *, *, #1888, .F. ) ;
#2321=DIRECTION ( 'NONE',  ( 0.000000000000000000, -1.000000000000000000, 0.000000000000000000 ) ) ;
#2360=VERTEX_POINT ( 'NONE', #13102 ) ;
#2403=EDGE_CURVE ( 'NONE', #5979, #8568, #16842, .T. ) ;
#2412=DIRECTION ( 'NONE',  ( -1.000000000000000000, 0.000000000000000000, 0.000000000000000000 ) ) ;
#2527=EDGE_CURVE ( 'NONE', #6481, #19827, #11887, .T. ) ;
#2560=AXIS2_PLACEMENT_3D ( 'NONE', #21515, #41440, #41189 ) ;
#2604=CARTESIAN_POINT ( 'NONE',  ( 30.68460988201149675, -15.41618894468000356, -65.65000000000004832 ) ) ;
#2613=EDGE_CURVE ( 'NONE', #6636, #14944, #35275, .T. ) ;
#2683=CARTESIAN_POINT ( 'NONE',  ( 68.13393739769618662, -29.16618894467940137, -65.65000000000000568 ) ) ;
#2699=CARTESIAN_POINT ( 'NONE',  ( 68.13393739769618662, -1.666188944679350081, -65.65000000000000568 ) ) ;
#2844=EDGE_CURVE ( 'NONE', #29283, #50827, #32741, .T. ) ;
#2864=CARTESIAN_POINT ( 'NONE',  ( 68.13393739823651174, -1.166188944679350081, -49.64999999999999858 ) ) ;
#2950=CARTESIAN_POINT ( 'NONE',  ( 68.13393739769618662, -15.41618894467939782, -65.65000000000000568 ) ) ;
#2967=DIRECTION ( 'NONE',  ( 0.000000000000000000, 0.000000000000000000, -1.000000000000000000 ) ) ;
#3047=CIRCLE ( 'NONE', #39905, 16.00000000000000000 ) ;
#3100=CARTESIAN_POINT ( 'NONE',  ( 68.13393739769618662, -0.5161889446793590519, -65.65000000000000568 ) ) ;
#3264=CARTESIAN_POINT ( 'NONE',  ( 31.58225770014201572, -28.80002732852027947, -29.09832030244561807 ) ) ;
#3349=AXIS2_PLACEMENT_3D ( 'NONE', #48071, #12169, #32553 ) ;
#3528=CARTESIAN_POINT ( 'NONE',  ( 105.5832649133809156, -15.41618894467909051, -28.20067248431509199 ) ) ;
#3569=DIRECTION ( 'NONE',  ( 0.000000000000000000, -1.000000000000000000, 0.000000000000000000 ) ) ;
#3601=ORIENTED_EDGE ( 'NONE', *, *, #16653, .F. ) ;
#3689=CARTESIAN_POINT ( 'NONE',  ( 67.48834183618497207, -5.818188944679350882, -65.18094736867061556 ) ) ;
#3690=PLANE ( 'NONE',  #47627 ) ;
#3740=AXIS2_PLACEMENT_3D ( 'NONE', #18177, #33376, #21062 ) ;
#3797=DIRECTION ( 'NONE',  ( 0.000000000000000000, 0.000000000000000000, -1.000000000000000000 ) ) ;
#4050=CARTESIAN_POINT ( 'NONE',  ( 68.13393739769618662, -15.41618894467939782, -65.65000000000000568 ) ) ;
#4071=EDGE_CURVE ( 'NONE', #18887, #27054, #50936, .T. ) ;
#4099=ORIENTED_EDGE ( 'NONE', *, *, #44191, .T. ) ;
#4132=CARTESIAN_POINT ( 'NONE',  ( 97.41201884798559263, -30.66618894467940137, -65.65000000000000568 ) ) ;
#4154=DIRECTION ( 'NONE',  ( 0.000000000000000000, -1.000000000000000000, 0.000000000000000000 ) ) ;
#4207=CARTESIAN_POINT ( 'NONE',  ( 68.13393739769618662, -30.31618894467939995, -81.65000000000000568 ) ) ;
#4254=SHAPE_REPRESENTATION_RELATIONSHIP ( 'NONE' , 'NONE' ,  #49550, #12204 ) ;
#4284=CARTESIAN_POINT ( 'NONE',  ( 68.13393739769658453, -28.80002732851820468, -102.2016796975550079 ) ) ;
#4323=DIRECTION ( 'NONE',  ( 1.000000000000000000, 0.000000000000000000, 0.000000000000000000 ) ) ;
#4453=CARTESIAN_POINT ( 'NONE',  ( 68.13393739769618662, -1.666188944679350081, -65.65000000000000568 ) ) ;
#4468=EDGE_CURVE ( 'NONE', #42029, #6481, #14979, .T. ) ;
#4483=FACE_OUTER_BOUND ( 'NONE', #38412, .T. ) ;
#4507=( NAMED_UNIT ( * ) PLANE_ANGLE_UNIT ( ) SI_UNIT ( $, .RADIAN. ) );
#4606=DIRECTION ( 'NONE',  ( 6.073366656256538404E-31, 1.365304166073849981E-11, -1.000000000000000000 ) ) ;
#4621=ORIENTED_EDGE ( 'NONE', *, *, #27776, .T. ) ;
#4622=EDGE_LOOP ( 'NONE', ( #484, #25916 ) ) ;
#4739=DIRECTION ( 'NONE',  ( 0.000000000000000000, -1.000000000000000000, 0.000000000000000000 ) ) ;
#4758=CARTESIAN_POINT ( 'NONE',  ( 68.13393739769627189, -15.41618894467850254, -103.0993275156849194 ) ) ;
#4774=EDGE_CURVE ( 'NONE', #31931, #24462, #23372, .T. ) ;
#4802=DIRECTION ( 'NONE',  ( 0.000000000000000000, -1.000000000000000000, 0.000000000000000000 ) ) ;
#4862=CARTESIAN_POINT ( 'NONE',  ( 68.77953295920740118, -25.01418894467940035, -65.18094736867061556 ) ) ;
#4906=CARTESIAN_POINT ( 'NONE',  ( 68.13393739769618662, 0.9838110553206419473, -65.65000000000000568 ) ) ;
#4952=FACE_OUTER_BOUND ( 'NONE', #12439, .T. ) ;
#5039=CIRCLE ( 'NONE', #3349, 16.00000000000000000 ) ;
#5116=CIRCLE ( 'NONE', #20984, 1.500000000000001332 ) ;
#5181=DIRECTION ( 'NONE',  ( 0.000000000000000000, -1.000000000000000000, 0.000000000000000000 ) ) ;
#5214=ORIENTED_EDGE ( 'NONE', *, *, #16566, .T. ) ;
#5297=EDGE_LOOP ( 'NONE', ( #15399, #9848 ) ) ;
#5345=DIRECTION ( 'NONE',  ( -1.000000000000000000, 0.000000000000000000, 0.000000000000000000 ) ) ;
#5407=EDGE_LOOP ( 'NONE', ( #19021, #38205, #4099, #13285 ) ) ;
#5450=CARTESIAN_POINT ( 'NONE',  ( 68.13393739769618662, -29.66618894467940137, -65.65000000000000568 ) ) ;
#5481=CYLINDRICAL_SURFACE ( 'NONE', #32307, 16.00000000000000000 ) ;
#5486=ORIENTED_EDGE ( 'NONE', *, *, #44191, .F. ) ;
#5517=EDGE_CURVE ( 'NONE', #29730, #34663, #21727, .T. ) ;
#5548=CARTESIAN_POINT ( 'NONE',  ( 68.13393739769618662, -2.032350560841069687, -29.09832030244572820 ) ) ;
#5560=CIRCLE ( 'NONE', #23106, 16.00000000000000000 ) ;
#5658=ORIENTED_EDGE ( 'NONE', *, *, #15743, .T. ) ;
#5708=CARTESIAN_POINT ( 'NONE',  ( 68.13393739769618662, -0.5161889446793590519, -81.65000000000000568 ) ) ;
#5738=ORIENTED_EDGE ( 'NONE', *, *, #33227, .F. ) ;
#5775=AXIS2_PLACEMENT_3D ( 'NONE', #6244, #10174, #17771 ) ;
#5854=DIRECTION ( 'NONE',  ( -1.000000000000000000, 0.000000000000000000, 0.000000000000000000 ) ) ;
#5861=ORIENTED_EDGE ( 'NONE', *, *, #48203, .T. ) ;
#5908=ORIENTED_EDGE ( 'NONE', *, *, #984, .F. ) ;
#5928=CIRCLE ( 'NONE', #35204, 6.099999999999994316 ) ;
#5945=EDGE_CURVE ( 'NONE', #32513, #43185, #10797, .T. ) ;
#5955=AXIS2_PLACEMENT_3D ( 'NONE', #4050, #36008, #43887 ) ;
#5975=EDGE_CURVE ( 'NONE', #28663, #50827, #47643, .T. ) ;
#5979=VERTEX_POINT ( 'NONE', #9412 ) ;
#5980=ORIENTED_EDGE ( 'NONE', *, *, #11423, .F. ) ;
#6011=DIRECTION ( 'NONE',  ( 0.000000000000000000, -1.000000000000000000, 0.000000000000000000 ) ) ;
#6023=DIRECTION ( 'NONE',  ( -1.000000000000000000, -1.681650659181820092E-11, -3.734562218117174162E-22 ) ) ;
#6058=ORIENTED_EDGE ( 'NONE', *, *, #30272, .T. ) ;
#6089=ORIENTED_EDGE ( 'NONE', *, *, #42242, .T. ) ;
#6112=DIRECTION ( 'NONE',  ( 1.965094753941435058E-11, -1.000000000000000000, 0.000000000000000000 ) ) ;
#6146=TOROIDAL_SURFACE ( 'NONE', #40430, 14.50000000000000000, 1.500000000000000000 ) ;
#6244=CARTESIAN_POINT ( 'NONE',  ( 68.13393739769618662, -29.66618894467940137, -90.65000000000000568 ) ) ;
#6274=ADVANCED_FACE ( 'NONE', ( #45632 ), #33373, .F. ) ;
#6292=ORIENTED_EDGE ( 'NONE', *, *, #24812, .T. ) ;
#6377=ORIENTED_EDGE ( 'NONE', *, *, #48561, .T. ) ;
#6396=DIRECTION ( 'NONE',  ( 2.448986521869468475E-28, 2.813979115193090436E-11, -1.000000000000000000 ) ) ;
#6448=CIRCLE ( 'NONE', #39889, 7.599999999999996092 ) ;
#6481=VERTEX_POINT ( 'NONE', #47701 ) ;
#6636=VERTEX_POINT ( 'NONE', #20925 ) ;
#6723=DIRECTION ( 'NONE',  ( 0.000000000000000000, -1.000000000000000000, 0.000000000000000000 ) ) ;
#6750=DIRECTION ( 'NONE',  ( 0.000000000000000000, -1.000000000000000000, 0.000000000000000000 ) ) ;
#6777=VERTEX_POINT ( 'NONE', #48143 ) ;
#6825=ORIENTED_EDGE ( 'NONE', *, *, #4071, .F. ) ;
#6835=TOROIDAL_SURFACE ( 'NONE', #21846, 14.50000000000000000, 1.500000000000000000 ) ;
#6880=DIRECTION ( 'NONE',  ( 0.000000000000000000, -1.000000000000000000, 0.000000000000000000 ) ) ;
#6907=FACE_OUTER_BOUND ( 'NONE', #32856, .T. ) ;
#6924=EDGE_CURVE ( 'NONE', #10836, #31099, #23368, .T. ) ;
#6927=EDGE_CURVE ( 'NONE', #17717, #18887, #22555, .T. ) ;
#7060=CARTESIAN_POINT ( 'NONE',  ( 68.13393739769618662, -31.81618894467930403, -80.15000000000000568 ) ) ;
#7069=ORIENTED_EDGE ( 'NONE', *, *, #27435, .F. ) ;
#7083=ORIENTED_EDGE ( 'NONE', *, *, #42880, .T. ) ;
#7101=TOROIDAL_SURFACE ( 'NONE', #17114, 34.55616290057869833, 2.000000000000000000 ) ;
#7111=DIRECTION ( 'NONE',  ( 0.000000000000000000, -1.000000000000000000, 0.000000000000000000 ) ) ;
#7277=AXIS2_PLACEMENT_3D ( 'NONE', #1339, #28843, #3797 ) ;
#7335=ORIENTED_EDGE ( 'NONE', *, *, #46144, .F. ) ;
#7360=DIRECTION ( 'NONE',  ( 0.000000000000000000, -1.000000000000000000, 0.000000000000000000 ) ) ;
#7406=ADVANCED_FACE ( 'NONE', ( #15451 ), #32556, .F. ) ;
#7412=DIRECTION ( 'NONE',  ( 0.000000000000000000, -1.000000000000000000, 0.000000000000000000 ) ) ;
#7433=AXIS2_PLACEMENT_3D ( 'NONE', #16862, #4802, #41738 ) ;
#7455=CARTESIAN_POINT ( 'NONE',  ( 104.6856170952509757, -28.80002732851738045, -102.2016796975550079 ) ) ;
#7491=CIRCLE ( 'NONE', #33435, 0.4999999999096970127 ) ;
#7566=AXIS2_PLACEMENT_3D ( 'NONE', #34725, #35516, #31559 ) ;
#7570=ADVANCED_FACE ( 'NONE', ( #45812 ), #20362, .F. ) ;
#7627=ORIENTED_EDGE ( 'NONE', *, *, #33913, .T. ) ;
#7672=CARTESIAN_POINT ( 'NONE',  ( 68.13393739769618662, -30.66618894467940137, -31.09383709942130380 ) ) ;
#7687=( NAMED_UNIT ( * ) SI_UNIT ( $, .STERADIAN. ) SOLID_ANGLE_UNIT ( ) );
#7694=AXIS2_PLACEMENT_3D ( 'NONE', #20021, #28402, #48085 ) ;
#7709=CARTESIAN_POINT ( 'NONE',  ( 68.13393739845098196, -29.66618894551239904, -65.65000000119469803 ) ) ;
#7729=TOROIDAL_SURFACE ( 'NONE', #12729, 23.49999999909039872, 0.4999999999562930175 ) ;
#7734=EDGE_LOOP ( 'NONE', ( #17522, #34315, #14388, #44515, #6089 ) ) ;
#7773=VERTEX_POINT ( 'NONE', #38200 ) ;
#7924=ORIENTED_EDGE ( 'NONE', *, *, #10767, .T. ) ;
#7927=DIRECTION ( 'NONE',  ( 1.000000000000000000, 0.000000000000000000, 0.000000000000000000 ) ) ;
#7954=ORIENTED_EDGE ( 'NONE', *, *, #28555, .F. ) ;
#7973=VERTEX_POINT ( 'NONE', #27164 ) ;
#7988=ORIENTED_EDGE ( 'NONE', *, *, #34222, .F. ) ;
#7992=ORIENTED_EDGE ( 'NONE', *, *, #12770, .F. ) ;
#8032=LINE ( 'NONE', #23983, #25954 ) ;
#8136=CARTESIAN_POINT ( 'NONE',  ( 68.13393739771808555, -29.66618894456289723, -82.15000000031059812 ) ) ;
#8153=ORIENTED_EDGE ( 'NONE', *, *, #38277, .F. ) ;
#8223=CARTESIAN_POINT ( 'NONE',  ( 30.68460988201149320, -15.41618894468070344, -28.20067248431509199 ) ) ;
#8236=ADVANCED_FACE ( 'NONE', ( #35365 ), #32135, .T. ) ;
#8240=AXIS2_PLACEMENT_3D ( 'NONE', #32975, #20666, #41373 ) ;
#8259=ORIENTED_EDGE ( 'NONE', *, *, #15289, .T. ) ;
#8411=AXIS2_PLACEMENT_3D ( 'NONE', #4132, #25056, #8849 ) ;
#8446=ORIENTED_EDGE ( 'NONE', *, *, #28555, .T. ) ;
#8476=CARTESIAN_POINT ( 'NONE',  ( 68.13393739769618662, -0.5161889446793590519, -65.65000000000000568 ) ) ;
#8531=UNCERTAINTY_MEASURE_WITH_UNIT (LENGTH_MEASURE( 1.000000000000000082E-05 ), #23837, 'distance_accuracy_value', 'NONE');
#8568=VERTEX_POINT ( 'NONE', #32279 ) ;
#8606=TOROIDAL_SURFACE ( 'NONE', #51302, 14.50000000000000000, 1.500000000000000000 ) ;
#8608=DIRECTION ( 'NONE',  ( -1.000000000000000000, 0.000000000000000000, 0.000000000000000000 ) ) ;
#8716=AXIS2_PLACEMENT_3D ( 'NONE', #49092, #40948, #32798 ) ;
#8722=ORIENTED_EDGE ( 'NONE', *, *, #291, .F. ) ;
#8797=DIRECTION ( 'NONE',  ( 0.000000000000000000, -1.000000000000000000, 0.000000000000000000 ) ) ;
#8800=ADVANCED_FACE ( 'NONE', ( #16849 ), #50583, .F. ) ;
#8841=DIRECTION ( 'NONE',  ( 0.000000000000000000, -1.000000000000000000, 0.000000000000000000 ) ) ;
#8849=DIRECTION ( 'NONE',  ( 0.000000000000000000, 0.000000000000000000, -1.000000000000000000 ) ) ;
#8927=SURFACE_STYLE_FILL_AREA ( #44044 ) ;
#8992=DIRECTION ( 'NONE',  ( 0.000000000000000000, 1.000000000000000000, 0.000000000000000000 ) ) ;
#9128=DIRECTION ( 'NONE',  ( 1.000000000000000000, 0.000000000000000000, -1.224646799147353207E-16 ) ) ;
#9172=EDGE_CURVE ( 'NONE', #48087, #42029, #17142, .T. ) ;
#9184=DIRECTION ( 'NONE',  ( 6.073366656256538404E-31, 1.365304166073849981E-11, -1.000000000000000000 ) ) ;
#9202=DIRECTION ( 'NONE',  ( -1.000000000000000000, 0.000000000000000000, 0.000000000000000000 ) ) ;
#9205=ORIENTED_EDGE ( 'NONE', *, *, #39841, .T. ) ;
#9232=CARTESIAN_POINT ( 'NONE',  ( 74.23393739769618094, -15.41618894467939782, -65.65000000000000568 ) ) ;
#9309=AXIS2_PLACEMENT_3D ( 'NONE', #16477, #40585, #24838 ) ;
#9329=CARTESIAN_POINT ( 'NONE',  ( 68.13393739769618662, -1.166188944679350081, -65.65000000000000568 ) ) ;
#9345=EDGE_LOOP ( 'NONE', ( #24704, #49448, #31982, #5658, #10371 ) ) ;
#9374=CIRCLE ( 'NONE', #50368, 0.5000000000336679573 ) ;
#9383=CARTESIAN_POINT ( 'NONE',  ( 88.13393739769618662, -29.16618894467940137, -65.65000000000000568 ) ) ;
#9412=CARTESIAN_POINT ( 'NONE',  ( 61.98540824044656006, 0.9838110553206419473, -61.18283208257727779 ) ) ;
#9446=DIRECTION ( 'NONE',  ( -1.000000000000000000, 0.000000000000000000, 0.000000000000000000 ) ) ;
#9608=DIRECTION ( 'NONE',  ( -1.000000000000000000, 0.000000000000000000, 0.000000000000000000 ) ) ;
#9656=CARTESIAN_POINT ( 'NONE',  ( 68.13393739769618662, -0.1661889446793599900, -100.2061629005786898 ) ) ;
#9726=EDGE_LOOP ( 'NONE', ( #29683, #31179, #38900, #42346, #49887 ) ) ;
#9844=DIRECTION ( 'NONE',  ( -3.191891195582396227E-12, 1.000000000000000000, 0.000000000000000000 ) ) ;
#9848=ORIENTED_EDGE ( 'NONE', *, *, #23796, .F. ) ;
#9882=CIRCLE ( 'NONE', #8240, 0.4999999999562930175 ) ;
#9899=CARTESIAN_POINT ( 'NONE',  ( 68.13393739769618662, -25.01418894467940035, -65.65000000000000568 ) ) ;
#9912=DIRECTION ( 'NONE',  ( -1.000000000000000000, 0.000000000000000000, 0.000000000000000000 ) ) ;
#9943=CARTESIAN_POINT ( 'NONE',  ( 104.6856170952509757, -28.80002732851810521, -65.65000000000000568 ) ) ;
#9989=DIRECTION ( 'NONE',  ( 0.000000000000000000, -1.000000000000000000, 0.000000000000000000 ) ) ;
#10020=ORIENTED_EDGE ( 'NONE', *, *, #1490, .F. ) ;
#10174=DIRECTION ( 'NONE',  ( -1.000000000000000000, -0.000000000000000000, -0.000000000000000000 ) ) ;
#10185=AXIS2_PLACEMENT_3D ( 'NONE', #44818, #37216, #29081 ) ;
#10193=AXIS2_PLACEMENT_3D ( 'NONE', #3100, #15405, #39252 ) ;
#10307=DIRECTION ( 'NONE',  ( -1.000000000000000000, 0.000000000000000000, 0.000000000000000000 ) ) ;
#10319=CARTESIAN_POINT ( 'NONE',  ( 68.13393739845098196, -29.66618894467940137, -89.64999999979866629 ) ) ;
#10357=DIRECTION ( 'NONE',  ( 0.000000000000000000, -1.000000000000000000, 0.000000000000000000 ) ) ;
#10371=ORIENTED_EDGE ( 'NONE', *, *, #2403, .F. ) ;
#10381=DIRECTION ( 'NONE',  ( 0.000000000000000000, 1.000000000000000000, 0.000000000000000000 ) ) ;
#10393=DIRECTION ( 'NONE',  ( -1.000000000000000000, 0.000000000000000000, 0.000000000000000000 ) ) ;
#10572=VERTEX_POINT ( 'NONE', #34274 ) ;
#10603=ORIENTED_EDGE ( 'NONE', *, *, #291, .T. ) ;
#10638=DIRECTION ( 'NONE',  ( 0.000000000000000000, -1.000000000000000000, 0.000000000000000000 ) ) ;
#10763=ORIENTED_EDGE ( 'NONE', *, *, #44287, .T. ) ;
#10767=EDGE_CURVE ( 'NONE', #8568, #5979, #43287, .T. ) ;
#10783=ORIENTED_EDGE ( 'NONE', *, *, #50470, .T. ) ;
#10797=CIRCLE ( 'NONE', #11661, 34.55616290057869833 ) ;
#10822=CARTESIAN_POINT ( 'NONE',  ( 68.13393739769618662, -1.666188944679350081, -65.65000000000000568 ) ) ;
#10836=VERTEX_POINT ( 'NONE', #25054 ) ;
#10838=CIRCLE ( 'NONE', #14146, 14.49999999999999822 ) ;
#10863=AXIS2_PLACEMENT_3D ( 'NONE', #20896, #45281, #37662 ) ;
#10903=CARTESIAN_POINT ( 'NONE',  ( 68.13393739769618662, -28.66618894467939782, -31.09383709942130380 ) ) ;
#10958=ORIENTED_EDGE ( 'NONE', *, *, #4468, .T. ) ;
#11134=CARTESIAN_POINT ( 'NONE',  ( 30.68460988201149675, -15.41618894468000356, -65.65000000000004832 ) ) ;
#11295=ADVANCED_FACE ( 'NONE', ( #21981 ), #11660, .F. ) ;
#11321=ORIENTED_EDGE ( 'NONE', *, *, #1960, .T. ) ;
#11335=DIRECTION ( 'NONE',  ( 1.000000000000000000, 0.000000000000000000, 0.000000000000000000 ) ) ;
#11423=EDGE_CURVE ( 'NONE', #17025, #7773, #41764, .T. ) ;
#11553=EDGE_CURVE ( 'NONE', #20784, #31931, #746, .T. ) ;
#11605=FACE_OUTER_BOUND ( 'NONE', #7734, .T. ) ;
#11660=TOROIDAL_SURFACE ( 'NONE', #31699, 23.49999999909039872, 0.4999999999562930175 ) ;
#11661=AXIS2_PLACEMENT_3D ( 'NONE', #29804, #49504, #41362 ) ;
#11760=ORIENTED_EDGE ( 'NONE', *, *, #2527, .T. ) ;
#11887=CIRCLE ( 'NONE', #10193, 16.00000000000000000 ) ;
#11920=EDGE_LOOP ( 'NONE', ( #44031, #36119, #36322, #35953 ) ) ;
#11924=AXIS2_PLACEMENT_3D ( 'NONE', #20488, #49536, #23644 ) ;
#11965=LINE ( 'NONE', #4862, #24584 ) ;
#11985=DIRECTION ( 'NONE',  ( 0.000000000000000000, -1.000000000000000000, 0.000000000000000000 ) ) ;
#12105=CARTESIAN_POINT ( 'NONE',  ( 68.13393739769618662, -31.81618894467930403, -51.14999999999999858 ) ) ;
#12150=DIRECTION ( 'NONE',  ( 0.000000000000000000, -1.000000000000000000, 0.000000000000000000 ) ) ;
#12163=CARTESIAN_POINT ( 'NONE',  ( 68.13393739769598767, -2.032350560839250253, -102.2016796975539989 ) ) ;
#12169=DIRECTION ( 'NONE',  ( 0.000000000000000000, 1.000000000000000000, 0.000000000000000000 ) ) ;
#12204=ADVANCED_BREP_SHAPE_REPRESENTATION ( '', ( #43885, #20940 ), #20155 ) ;
#12212=FACE_OUTER_BOUND ( 'NONE', #617, .T. ) ;
#12404=CARTESIAN_POINT ( 'NONE',  ( 68.13393739769618662, -28.80002732851770020, -102.2016796975542690 ) ) ;
#12420=DIRECTION ( 'NONE',  ( 1.000000000000000000, 0.000000000000000000, -1.224646799147353207E-16 ) ) ;
#12439=EDGE_LOOP ( 'NONE', ( #7069, #6292, #41160, #47672, #43480, #37001 ) ) ;
#12480=FACE_OUTER_BOUND ( 'NONE', #16461, .T. ) ;
#12481=EDGE_CURVE ( 'NONE', #32513, #39247, #50223, .T. ) ;
#12554=EDGE_CURVE ( 'NONE', #19827, #14727, #5039, .T. ) ;
#12586=CARTESIAN_POINT ( 'NONE',  ( 79.93393739769618378, 0.9838110553206419473, -65.65000000000000568 ) ) ;
#12632=CARTESIAN_POINT ( 'NONE',  ( 68.13393739769618662, -28.80002732851770020, -29.09832030244573176 ) ) ;
#12660=EDGE_CURVE ( 'NONE', #27825, #36314, #25, .T. ) ;
#12699=TOROIDAL_SURFACE ( 'NONE', #23546, 16.49999999812870044, 0.4999999999096970127 ) ;
#12707=ORIENTED_EDGE ( 'NONE', *, *, #39393, .T. ) ;
#12729=AXIS2_PLACEMENT_3D ( 'NONE', #421, #171, #4606 ) ;
#12753=EDGE_LOOP ( 'NONE', ( #13575, #29230, #25023, #46231, #19392 ) ) ;
#12770=EDGE_CURVE ( 'NONE', #31099, #10836, #24253, .T. ) ;
#12787=FACE_OUTER_BOUND ( 'NONE', #51540, .T. ) ;
#12863=FILL_AREA_STYLE_COLOUR ( '', #44981 ) ;
#12891=CIRCLE ( 'NONE', #31252, 1.000000000000000888 ) ;
#13045=CIRCLE ( 'NONE', #17220, 25.00000000000000000 ) ;
#13102=CARTESIAN_POINT ( 'NONE',  ( 68.13393739771649393, -29.16618894460431477, -82.15000000015528769 ) ) ;
#13120=DIRECTION ( 'NONE',  ( 1.000000000000000000, 0.000000000000000000, 0.000000000000000000 ) ) ;
#13129=CARTESIAN_POINT ( 'NONE',  ( 68.13393739806078031, -1.166188945131049870, -65.65000000072619457 ) ) ;
#13200=CIRCLE ( 'NONE', #28232, 36.55167969755429880 ) ;
#13270=CARTESIAN_POINT ( 'NONE',  ( 68.13393739769618662, -2.032350560841069687, -29.09832030244572820 ) ) ;
#13285=ORIENTED_EDGE ( 'NONE', *, *, #2844, .F. ) ;
#13302=CARTESIAN_POINT ( 'NONE',  ( 68.13393739769618662, -0.1661889446793529956, -65.65000000000000568 ) ) ;
#13305=ORIENTED_EDGE ( 'NONE', *, *, #43080, .T. ) ;
#13424=AXIS2_PLACEMENT_3D ( 'NONE', #2699, #30203, #10307 ) ;
#13575=ORIENTED_EDGE ( 'NONE', *, *, #9172, .F. ) ;
#13633=CARTESIAN_POINT ( 'NONE',  ( 62.03393739769618520, -0.5161889446793590519, -65.65000000000000568 ) ) ;
#13700=DIRECTION ( 'NONE',  ( -1.000000000000000000, 0.000000000000000000, 0.000000000000000000 ) ) ;
#13717=EDGE_CURVE ( 'NONE', #10836, #31172, #7491, .T. ) ;
#13780=DIRECTION ( 'NONE',  ( 1.000000000000000000, 3.191443934968493537E-12, -1.224645901081695283E-16 ) ) ;
#13878=CARTESIAN_POINT ( 'NONE',  ( 31.58225770014188427, -28.80002732851970393, -65.65000000000000568 ) ) ;
#13879=CARTESIAN_POINT ( 'NONE',  ( 68.13393739769618662, -1.166188944679350081, -65.65000000000000568 ) ) ;
#13902=AXIS2_PLACEMENT_3D ( 'NONE', #31552, #10638, #26593 ) ;
#13937=DIRECTION ( 'NONE',  ( 0.000000000000000000, -1.000000000000000000, 0.000000000000000000 ) ) ;
#13959=AXIS2_PLACEMENT_3D ( 'NONE', #7709, #98, #32280 ) ;
#13981=VERTEX_POINT ( 'NONE', #503 ) ;
#13984=DIRECTION ( 'NONE',  ( 1.681650659181820092E-11, -1.000000000000000000, -2.220771714818679968E-11 ) ) ;
#13998=DIRECTION ( 'NONE',  ( 0.000000000000000000, 0.000000000000000000, 1.000000000000000000 ) ) ;
#14133=DIRECTION ( 'NONE',  ( 0.000000000000000000, -1.000000000000000000, 0.000000000000000000 ) ) ;
#14146=AXIS2_PLACEMENT_3D ( 'NONE', #41976, #13937, #2139 ) ;
#14198=DIRECTION ( 'NONE',  ( 1.000000000000000000, 0.000000000000000000, 0.000000000000000000 ) ) ;
#14253=CARTESIAN_POINT ( 'NONE',  ( 68.13393739806289773, -1.666188944679350081, -42.14999999999999858 ) ) ;
#14298=ORIENTED_EDGE ( 'NONE', *, *, #37139, .T. ) ;
#14375=ORIENTED_EDGE ( 'NONE', *, *, #28323, .T. ) ;
#14376=DIRECTION ( 'NONE',  ( 1.000000000000000000, 0.000000000000000000, 0.000000000000000000 ) ) ;
#14388=ORIENTED_EDGE ( 'NONE', *, *, #31026, .T. ) ;
#14392=CARTESIAN_POINT ( 'NONE',  ( 68.13393739769598767, -2.032350560840590070, -29.09832030244560741 ) ) ;
#14479=CIRCLE ( 'NONE', #50476, 16.50000000000000000 ) ;
#14508=DIRECTION ( 'NONE',  ( 3.191443934968489902E-12, -1.000000000000000000, -2.813979115193090113E-11 ) ) ;
#14541=ORIENTED_EDGE ( 'NONE', *, *, #27373, .T. ) ;
#14546=DIRECTION ( 'NONE',  ( 1.000000000000000000, 0.000000000000000000, 0.000000000000000000 ) ) ;
#14567=DIRECTION ( 'NONE',  ( 0.000000000000000000, 0.000000000000000000, -1.000000000000000000 ) ) ;
#14700=CARTESIAN_POINT ( 'NONE',  ( 68.13393739769618662, -30.49118894467929763, -65.65000000000000568 ) ) ;
#14709=AXIS2_PLACEMENT_3D ( 'NONE', #37804, #18388, #42776 ) ;
#14727=VERTEX_POINT ( 'NONE', #31884 ) ;
#14812=ORIENTED_EDGE ( 'NONE', *, *, #36920, .T. ) ;
#14835=FACE_OUTER_BOUND ( 'NONE', #50003, .T. ) ;
#14866=CARTESIAN_POINT ( 'NONE',  ( 68.13393739769618662, -29.66618894467940137, -65.65000000000000568 ) ) ;
#14892=EDGE_CURVE ( 'NONE', #1527, #44651, #20942, .T. ) ;
#14907=FACE_OUTER_BOUND ( 'NONE', #21852, .T. ) ;
#14944=VERTEX_POINT ( 'NONE', #48413 ) ;
#14974=AXIS2_PLACEMENT_3D ( 'NONE', #34070, #1865, #49830 ) ;
#14979=CIRCLE ( 'NONE', #37573, 16.00000000000000000 ) ;
#15078=VERTEX_POINT ( 'NONE', #18161 ) ;
#15084=CIRCLE ( 'NONE', #22622, 34.55616290057869833 ) ;
#15116=CIRCLE ( 'NONE', #7566, 2.000000000000001776 ) ;
#15138=DIRECTION ( 'NONE',  ( 0.000000000000000000, -1.000000000000000000, 0.000000000000000000 ) ) ;
#15150=ORIENTED_EDGE ( 'NONE', *, *, #19116, .T. ) ;
#15179=CARTESIAN_POINT ( 'NONE',  ( 68.13393739769618662, -29.66618894467940137, -65.65000000000000568 ) ) ;
#15225=DIRECTION ( 'NONE',  ( 1.000000000000000000, 0.000000000000000000, 0.000000000000000000 ) ) ;
#15289=EDGE_CURVE ( 'NONE', #24229, #48161, #15084, .T. ) ;
#15319=CARTESIAN_POINT ( 'NONE',  ( 104.6856170952509757, -28.80002732851879088, -29.09832030244561807 ) ) ;
#15377=VERTEX_POINT ( 'NONE', #1021 ) ;
#15399=ORIENTED_EDGE ( 'NONE', *, *, #46405, .F. ) ;
#15403=CONICAL_SURFACE ( 'NONE', #44682, 0.7980000000000000426, 0.7853981633974476129 ) ;
#15405=DIRECTION ( 'NONE',  ( 0.000000000000000000, 1.000000000000000000, 0.000000000000000000 ) ) ;
#15451=FACE_OUTER_BOUND ( 'NONE', #17840, .T. ) ;
#15604=VERTEX_POINT ( 'NONE', #19866 ) ;
#15621=TOROIDAL_SURFACE ( 'NONE', #50790, 16.49999999930319916, 0.5000000000336690675 ) ;
#15634=ORIENTED_EDGE ( 'NONE', *, *, #5975, .T. ) ;
#15651=CARTESIAN_POINT ( 'NONE',  ( 68.13393739769618662, -2.032350560841069687, -65.65000000000000568 ) ) ;
#15743=EDGE_CURVE ( 'NONE', #18887, #8568, #2223, .T. ) ;
#15906=AXIS2_PLACEMENT_3D ( 'NONE', #46491, #30214, #2967 ) ;
#15909=EDGE_CURVE ( 'NONE', #10572, #2360, #902, .T. ) ;
#15928=DIRECTION ( 'NONE',  ( 0.000000000000000000, 0.000000000000000000, -1.000000000000000000 ) ) ;
#16011=CARTESIAN_POINT ( 'NONE',  ( 84.13393739769618662, -30.31618894467939995, -65.65000000000000568 ) ) ;
#16014=( BOUNDED_SURFACE ( )  B_SPLINE_SURFACE ( 2, 2, ( 
 ( #45593, #25903, #21715, #25649, #37727, #42703, #26169, #46385, #14392 ),
 ( #34030, #22752, #2604, #38772, #49786, #42179, #45857, #18577, #50307 ),
 ( #1822, #30617, #13878, #29838, #50040, #30357, #9943, #41918, #38244 ) ),
 .UNSPECIFIED., .F., .T., .T. ) 
 B_SPLINE_SURFACE_WITH_KNOTS ( ( 3, 3 ),
 ( 3, 2, 2, 2, 3 ),
 ( -0.06696923885014899325, 0.06696923885011449307 ),
 ( -3.141592653589790007, -1.570796326794899889, 0.000000000000000000, 1.570796326794899889, 3.141592653589790007 ),
 .UNSPECIFIED. ) 
 GEOMETRIC_REPRESENTATION_ITEM ( )  RATIONAL_B_SPLINE_SURFACE ( (
 ( 1.000000000000000000, 0.7071067811865480168, 1.000000000000000000, 0.7071067811865480168, 1.000000000000000000, 0.7071067811865480168, 1.000000000000000000, 0.7071067811865480168, 1.000000000000000000),
 ( 0.9977583984878120038, 0.7055217295565610058, 0.9977583984878120038, 0.7055217295565610058, 0.9977583984878120038, 0.7055217295565610058, 0.9977583984878120038, 0.7055217295565610058, 0.9977583984878120038),
 ( 1.000000000000000000, 0.7071067811865480168, 1.000000000000000000, 0.7071067811865480168, 1.000000000000000000, 0.7071067811865480168, 1.000000000000000000, 0.7071067811865480168, 1.000000000000000000) ) ) 
 REPRESENTATION_ITEM ( '' )  SURFACE ( )  );
#16036=EDGE_CURVE ( 'NONE', #36314, #26336, #36051, .T. ) ;
#16041=CARTESIAN_POINT ( 'NONE',  ( 68.13393739769618662, -30.31618894467939995, -65.65000000000000568 ) ) ;
#16056=AXIS2_PLACEMENT_3D ( 'NONE', #42012, #34905, #6112 ) ;
#16082=CARTESIAN_POINT ( 'NONE',  ( 68.13393739769625768, -15.41618894467850076, -103.0993275156848910 ) ) ;
#16120=EDGE_LOOP ( 'NONE', ( #33359, #31971, #23332, #34074 ) ) ;
#16157=VECTOR ( 'NONE', #43610, 1000.000000000000000 ) ;
#16162=ORIENTED_EDGE ( 'NONE', *, *, #35076, .F. ) ;
#16177=FACE_OUTER_BOUND ( 'NONE', #51492, .T. ) ;
#16183=FACE_BOUND ( 'NONE', #28077, .T. ) ;
#16187=AXIS2_PLACEMENT_3D ( 'NONE', #9899, #48712, #17256 ) ;
#16189=DIRECTION ( 'NONE',  ( 1.000000000000000000, 0.000000000000000000, 0.000000000000000000 ) ) ;
#16253=DIRECTION ( 'NONE',  ( -1.681987882033212302E-11, 1.000000000000000000, 0.000000000000000000 ) ) ;
#16270=DIRECTION ( 'NONE',  ( 0.000000000000000000, 0.000000000000000000, -1.000000000000000000 ) ) ;
#16281=DIRECTION ( 'NONE',  ( 1.000000000000000000, 0.000000000000000000, 0.000000000000000000 ) ) ;
#16364=AXIS2_PLACEMENT_3D ( 'NONE', #1557, #6011, #48747 ) ;
#16400=ORIENTED_EDGE ( 'NONE', *, *, #389, .F. ) ;
#16461=EDGE_LOOP ( 'NONE', ( #27008, #50407, #6377, #48421 ) ) ;
#16477=CARTESIAN_POINT ( 'NONE',  ( 68.13393739769618662, -30.66618894467940137, -65.65000000000000568 ) ) ;
#16564=DIRECTION ( 'NONE',  ( 1.000000000000000000, 0.000000000000000000, 0.000000000000000000 ) ) ;
#16566=EDGE_CURVE ( 'NONE', #6481, #25686, #23533, .T. ) ;
#16621=DIRECTION ( 'NONE',  ( 0.8090169943749515591, 0.000000000000000000, -0.5877852522924675860 ) ) ;
#16653=EDGE_CURVE ( 'NONE', #28355, #29283, #46152, .T. ) ;
#16672=DIRECTION ( 'NONE',  ( 1.000000000000000000, 0.000000000000000000, 0.000000000000000000 ) ) ;
#16746=CARTESIAN_POINT ( 'NONE',  ( 68.13393739769618662, -31.81618894467930403, -65.65000000000000568 ) ) ;
#16779=CARTESIAN_POINT ( 'NONE',  ( 68.13393739769618662, -30.31618894467939995, -65.65000000000000568 ) ) ;
#16818=CARTESIAN_POINT ( 'NONE',  ( 68.13393739769618662, -2.032350560841069687, -102.2016796975542690 ) ) ;
#16831=ORIENTED_EDGE ( 'NONE', *, *, #37139, .F. ) ;
#16842=CIRCLE ( 'NONE', #43642, 7.599999999999996092 ) ;
#16849=FACE_OUTER_BOUND ( 'NONE', #24323, .T. ) ;
#16857=CARTESIAN_POINT ( 'NONE',  ( 68.13393739769618662, -0.5161889446793590519, -49.64999999999999858 ) ) ;
#16862=CARTESIAN_POINT ( 'NONE',  ( 68.13393739769618662, -0.5161889446793590519, -65.65000000000000568 ) ) ;
#16927=DIRECTION ( 'NONE',  ( 0.000000000000000000, 0.000000000000000000, -1.000000000000000000 ) ) ;
#16995=AXIS2_PLACEMENT_3D ( 'NONE', #33212, #44505, #8608 ) ;
#16998=ORIENTED_EDGE ( 'NONE', *, *, #19351, .F. ) ;
#17018=DIRECTION ( 'NONE',  ( 0.000000000000000000, -1.000000000000000000, 0.000000000000000000 ) ) ;
#17025=VERTEX_POINT ( 'NONE', #39232 ) ;
#17047=PRESENTATION_STYLE_ASSIGNMENT (( #48758 ) ) ;
#17114=AXIS2_PLACEMENT_3D ( 'NONE', #44737, #8841, #15928 ) ;
#17142=CIRCLE ( 'NONE', #31357, 1.500000000000001332 ) ;
#17201=EDGE_LOOP ( 'NONE', ( #8722, #39517 ) ) ;
#17220=AXIS2_PLACEMENT_3D ( 'NONE', #38731, #42660, #37684 ) ;
#17256=DIRECTION ( 'NONE',  ( 0.8090169943749515591, 0.000000000000000000, 0.5877852522924675860 ) ) ;
#17273=CARTESIAN_POINT ( 'NONE',  ( 68.13393739769618662, -30.31618894467939995, -65.65000000000000568 ) ) ;
#17274=DIRECTION ( 'NONE',  ( 0.000000000000000000, -1.000000000000000000, 0.000000000000000000 ) ) ;
#17304=AXIS2_PLACEMENT_3D ( 'NONE', #41548, #26067, #37888 ) ;
#17321=ADVANCED_FACE ( 'NONE', ( #23346 ), #12699, .F. ) ;
#17349=EDGE_CURVE ( 'NONE', #7773, #10572, #9374, .T. ) ;
#17400=( BOUNDED_SURFACE ( )  B_SPLINE_SURFACE ( 2, 2, ( 
 ( #48064, #28119, #32041, #51480, #12163, #27868, #44125, #23916, #23408 ),
 ( #39941, #8223, #11134, #43619, #16082, #39428, #31790, #3528, #27613 ),
 ( #19499, #3264, #50957, #40194, #4284, #7455, #47047, #15319, #34958 ) ),
 .UNSPECIFIED., .F., .T., .T. ) 
 B_SPLINE_SURFACE_WITH_KNOTS ( ( 3, 3 ),
 ( 3, 2, 2, 2, 3 ),
 ( -0.06696923885014899325, 0.06696923885011449307 ),
 ( -3.141592653589790007, -1.570796326794899889, 0.000000000000000000, 1.570796326794899889, 3.141592653589790007 ),
 .UNSPECIFIED. ) 
 GEOMETRIC_REPRESENTATION_ITEM ( )  RATIONAL_B_SPLINE_SURFACE ( (
 ( 1.000000000000000000, 0.7071067811865480168, 1.000000000000000000, 0.7071067811865480168, 1.000000000000000000, 0.7071067811865480168, 1.000000000000000000, 0.7071067811865480168, 1.000000000000000000),
 ( 0.9977583984878120038, 0.7055217295565610058, 0.9977583984878120038, 0.7055217295565610058, 0.9977583984878120038, 0.7055217295565610058, 0.9977583984878120038, 0.7055217295565610058, 0.9977583984878120038),
 ( 1.000000000000000000, 0.7071067811865480168, 1.000000000000000000, 0.7071067811865480168, 1.000000000000000000, 0.7071067811865480168, 1.000000000000000000, 0.7071067811865480168, 1.000000000000000000) ) ) 
 REPRESENTATION_ITEM ( '' )  SURFACE ( )  );
#17521=AXIS2_PLACEMENT_3D ( 'NONE', #23402, #50446, #23662 ) ;
#17522=ORIENTED_EDGE ( 'NONE', *, *, #12660, .T. ) ;
#17591=CARTESIAN_POINT ( 'NONE',  ( 68.13393739769618662, -28.80002732851770020, -102.2016796975542690 ) ) ;
#17602=DIRECTION ( 'NONE',  ( 0.000000000000000000, -1.000000000000000000, 0.000000000000000000 ) ) ;
#17716=ORIENTED_EDGE ( 'NONE', *, *, #20845, .F. ) ;
#17717=VERTEX_POINT ( 'NONE', #13633 ) ;
#17743=ADVANCED_FACE ( 'NONE', ( #45596 ), #35273, .T. ) ;
#17771=DIRECTION ( 'NONE',  ( 0.000000000000000000, 0.000000000000000000, 1.000000000000000000 ) ) ;
#17840=EDGE_LOOP ( 'NONE', ( #40722, #5861, #10763, #17716, #5908 ) ) ;
#17863=EDGE_CURVE ( 'NONE', #36314, #6777, #49594, .T. ) ;
#17957=CARTESIAN_POINT ( 'NONE',  ( 68.13393739823159478, -1.166188945610419969, -65.65000000186969942 ) ) ;
#18161=CARTESIAN_POINT ( 'NONE',  ( 68.13393739769618662, -0.1661889446793515246, -40.64999999999999858 ) ) ;
#18177=CARTESIAN_POINT ( 'NONE',  ( 68.13393739769618662, -29.66618894467940137, -65.65000000000000568 ) ) ;
#18200=CARTESIAN_POINT ( 'NONE',  ( 68.77953295920740118, -5.818188944679350882, -66.11905263132939581 ) ) ;
#18212=ORIENTED_EDGE ( 'NONE', *, *, #51310, .F. ) ;
#18388=DIRECTION ( 'NONE',  ( 0.000000000000000000, 1.000000000000000000, 0.000000000000000000 ) ) ;
#18493=ORIENTED_EDGE ( 'NONE', *, *, #20845, .T. ) ;
#18557=DIRECTION ( 'NONE',  ( -1.000000000000000000, 0.000000000000000000, 0.000000000000000000 ) ) ;
#18573=ORIENTED_EDGE ( 'NONE', *, *, #17349, .T. ) ;
#18577=CARTESIAN_POINT ( 'NONE',  ( 105.5832649133809156, -15.41618894467909051, -28.20067248431509199 ) ) ;
#18627=FACE_OUTER_BOUND ( 'NONE', #26992, .T. ) ;
#18675=ORIENTED_EDGE ( 'NONE', *, *, #11553, .F. ) ;
#18694=DIRECTION ( 'NONE',  ( 1.000000000000000000, 0.000000000000000000, 0.000000000000000000 ) ) ;
#18718=DIRECTION ( 'NONE',  ( 0.000000000000000000, -1.000000000000000000, 0.000000000000000000 ) ) ;
#18867=DIRECTION ( 'NONE',  ( 1.000000000000000000, 0.000000000000000000, 0.000000000000000000 ) ) ;
#18887=VERTEX_POINT ( 'NONE', #20339 ) ;
#18920=DIRECTION ( 'NONE',  ( 0.000000000000000000, -1.000000000000000000, 0.000000000000000000 ) ) ;
#18947=ORIENTED_EDGE ( 'NONE', *, *, #31026, .F. ) ;
#18961=ORIENTED_EDGE ( 'NONE', *, *, #11553, .T. ) ;
#19021=ORIENTED_EDGE ( 'NONE', *, *, #39841, .F. ) ;
#19076=ADVANCED_FACE ( 'NONE', ( #47798 ), #6146, .T. ) ;
#19116=EDGE_CURVE ( 'NONE', #17025, #6777, #27605, .T. ) ;
#19351=EDGE_CURVE ( 'NONE', #2360, #10572, #14479, .T. ) ;
#19392=ORIENTED_EDGE ( 'NONE', *, *, #27435, .T. ) ;
#19408=APPLICATION_CONTEXT ( 'automotive_design' ) ;
#19499=CARTESIAN_POINT ( 'NONE',  ( 68.13393739769658453, -28.80002732851960445, -29.09832030244560741 ) ) ;
#19504=CARTESIAN_POINT ( 'NONE',  ( 68.13393739769618662, -1.166188944679350081, -65.65000000000000568 ) ) ;
#19570=ORIENTED_EDGE ( 'NONE', *, *, #46405, .T. ) ;
#19613=CIRCLE ( 'NONE', #3740, 16.00000000000000000 ) ;
#19658=TOROIDAL_SURFACE ( 'NONE', #36359, 34.55616290057869833, 2.000000000000000000 ) ;
#19660=CARTESIAN_POINT ( 'NONE',  ( 88.13393739769618662, -1.666188944679350081, -65.65000000000000568 ) ) ;
#19728=EDGE_CURVE ( 'NONE', #7973, #40265, #1090, .T. ) ;
#19781=DIRECTION ( 'NONE',  ( 1.000000000000000000, 0.000000000000000000, -1.224646799147353207E-16 ) ) ;
#19827=VERTEX_POINT ( 'NONE', #5708 ) ;
#19831=CARTESIAN_POINT ( 'NONE',  ( 68.13393739769618662, -28.80002732851770020, -65.65000000000000568 ) ) ;
#19850=ADVANCED_FACE ( 'NONE', ( #50254 ), #32068, .T. ) ;
#19866=CARTESIAN_POINT ( 'NONE',  ( 74.23393739769618094, -30.31618894467939995, -65.65000000000000568 ) ) ;
#19875=CARTESIAN_POINT ( 'NONE',  ( 84.13393739769618662, -0.3411889446793609504, -65.65000000000000568 ) ) ;
#19953=ORIENTED_EDGE ( 'NONE', *, *, #49823, .T. ) ;
#20012=ORIENTED_EDGE ( 'NONE', *, *, #51305, .T. ) ;
#20021=CARTESIAN_POINT ( 'NONE',  ( 97.41201884798559263, -0.1661889446793529956, -65.65000000000000568 ) ) ;
#20078=TOROIDAL_SURFACE ( 'NONE', #15906, 25.00000000000000000, 1.000000000000000000 ) ;
#20155=( GEOMETRIC_REPRESENTATION_CONTEXT ( 3 ) GLOBAL_UNCERTAINTY_ASSIGNED_CONTEXT ( ( #43150 ) ) GLOBAL_UNIT_ASSIGNED_CONTEXT ( ( #32260, #4507, #7687 ) ) REPRESENTATION_CONTEXT ( 'NONE', 'WORKASPACE' ) );
#20202=CARTESIAN_POINT ( 'NONE',  ( 68.13393739769618662, -0.3411889446793609504, -65.65000000000000568 ) ) ;
#20246=DIRECTION ( 'NONE',  ( 0.000000000000000000, 0.000000000000000000, -1.000000000000000000 ) ) ;
#20282=ORIENTED_EDGE ( 'NONE', *, *, #12554, .F. ) ;
#20305=AXIS2_PLACEMENT_3D ( 'NONE', #49413, #1959, #46255 ) ;
#20324=ORIENTED_EDGE ( 'NONE', *, *, #9172, .T. ) ;
#20334=AXIS2_PLACEMENT_3D ( 'NONE', #38171, #46305, #10393 ) ;
#20339=CARTESIAN_POINT ( 'NONE',  ( 73.06894106338337735, -0.5161889446793590519, -69.23549003898403953 ) ) ;
#20359=PLANE ( 'NONE',  #8411 ) ;
#20362=CONICAL_SURFACE ( 'NONE', #16187, 0.7980000000000000426, 0.7853981633974476129 ) ;
#20488=CARTESIAN_POINT ( 'NONE',  ( 68.13393739769618662, -31.81618894467930403, -65.65000000000000568 ) ) ;
#20606=CIRCLE ( 'NONE', #17304, 2.000000000000001776 ) ;
#20640=AXIS2_PLACEMENT_3D ( 'NONE', #1014, #238, #36382 ) ;
#20666=DIRECTION ( 'NONE',  ( 1.000000000000000000, 8.402539340422012971E-12, -1.224645651945156590E-16 ) ) ;
#20779=CARTESIAN_POINT ( 'NONE',  ( 68.13393739769618662, -30.31618894467939995, -65.65000000000000568 ) ) ;
#20784=VERTEX_POINT ( 'NONE', #31584 ) ;
#20845=EDGE_CURVE ( 'NONE', #20784, #47321, #11965, .T. ) ;
#20879=CARTESIAN_POINT ( 'NONE',  ( 68.13393739806078031, -1.166188944810203409, -89.14999999981660039 ) ) ;
#20896=CARTESIAN_POINT ( 'NONE',  ( 68.13393739769618662, -1.166188944679350081, -65.65000000000000568 ) ) ;
#20907=AXIS2_PLACEMENT_3D ( 'NONE', #10822, #50650, #5854 ) ;
#20925=CARTESIAN_POINT ( 'NONE',  ( 84.13393739769618662, -29.66618894467940137, -65.65000000000000568 ) ) ;
#20940=AXIS2_PLACEMENT_3D ( 'NONE', #26546, #22357, #18694 ) ;
#20942=CIRCLE ( 'NONE', #26817, 0.4999999999562930175 ) ;
#20971=ADVANCED_FACE ( 'NONE', ( #43923, #12212 ), #32093, .T. ) ;
#20984=AXIS2_PLACEMENT_3D ( 'NONE', #25044, #1488, #24788 ) ;
#21062=DIRECTION ( 'NONE',  ( -1.000000000000000000, 0.000000000000000000, 0.000000000000000000 ) ) ;
#21082=AXIS2_PLACEMENT_3D ( 'NONE', #16779, #32728, #9446 ) ;
#21373=EDGE_LOOP ( 'NONE', ( #42341, #13305, #42865, #14298, #33158 ) ) ;
#21469=AXIS2_PLACEMENT_3D ( 'NONE', #45917, #25708, #14198 ) ;
#21515=CARTESIAN_POINT ( 'NONE',  ( 68.13393739769618662, -0.1661889446793599900, -65.65000000000000568 ) ) ;
#21638=ADVANCED_FACE ( 'NONE', ( #26911 ), #24404, .T. ) ;
#21715=CARTESIAN_POINT ( 'NONE',  ( 31.58225770014178835, -2.032350560840699760, -65.65000000000000568 ) ) ;
#21727=CIRCLE ( 'NONE', #51780, 16.00000000000000000 ) ;
#21755=ADVANCED_FACE ( 'NONE', ( #12480 ), #7729, .F. ) ;
#21846=AXIS2_PLACEMENT_3D ( 'NONE', #16041, #7412, #43573 ) ;
#21852=EDGE_LOOP ( 'NONE', ( #2285, #46418, #11321, #915 ) ) ;
#21981=FACE_OUTER_BOUND ( 'NONE', #37324, .T. ) ;
#22097=AXIS2_PLACEMENT_3D ( 'NONE', #44176, #8797, #16927 ) ;
#22162=AXIS2_PLACEMENT_3D ( 'NONE', #9329, #10357, #45741 ) ;
#22240=CIRCLE ( 'NONE', #14709, 25.00000000000000000 ) ;
#22314=AXIS2_PLACEMENT_3D ( 'NONE', #13879, #14133, #46386 ) ;
#22333=CIRCLE ( 'NONE', #20640, 16.00000000000000000 ) ;
#22351=LINE ( 'NONE', #36588, #44670 ) ;
#22353=ORIENTED_EDGE ( 'NONE', *, *, #17863, .F. ) ;
#22357=DIRECTION ( 'NONE',  ( 0.000000000000000000, 0.000000000000000000, 1.000000000000000000 ) ) ;
#22368=ORIENTED_EDGE ( 'NONE', *, *, #48203, .F. ) ;
#22453=CARTESIAN_POINT ( 'NONE',  ( 68.13393739845096775, -29.66618894467940137, -41.65000000139604452 ) ) ;
#22514=AXIS2_PLACEMENT_3D ( 'NONE', #46528, #18718, #34695 ) ;
#22549=CIRCLE ( 'NONE', #10863, 24.00000000000000000 ) ;
#22555=CIRCLE ( 'NONE', #44294, 6.099999999999994316 ) ;
#22622=AXIS2_PLACEMENT_3D ( 'NONE', #38806, #35107, #18867 ) ;
#22701=EDGE_LOOP ( 'NONE', ( #5980, #15150, #22353, #35440, #5738, #32644 ) ) ;
#22752=CARTESIAN_POINT ( 'NONE',  ( 30.68460988201149320, -15.41618894468070344, -28.20067248431509199 ) ) ;
#22898=CIRCLE ( 'NONE', #43868, 6.099999999999994316 ) ;
#23055=DIRECTION ( 'NONE',  ( -1.965094753941435058E-11, 1.000000000000000000, 0.000000000000000000 ) ) ;
#23106=AXIS2_PLACEMENT_3D ( 'NONE', #24629, #4739, #9202 ) ;
#23135=CIRCLE ( 'NONE', #49955, 16.00000000000000000 ) ;
#23160=CARTESIAN_POINT ( 'NONE',  ( 68.13393739769618662, -2.166188944679360073, -31.09383709942130380 ) ) ;
#23225=ORIENTED_EDGE ( 'NONE', *, *, #48561, .F. ) ;
#23332=ORIENTED_EDGE ( 'NONE', *, *, #43444, .F. ) ;
#23346=FACE_OUTER_BOUND ( 'NONE', #40455, .T. ) ;
#23368=CIRCLE ( 'NONE', #17521, 16.50000000000000000 ) ;
#23372=CIRCLE ( 'NONE', #35962, 6.099999999999994316 ) ;
#23381=CARTESIAN_POINT ( 'NONE',  ( 74.28246655494574213, -31.81618894467930403, -61.18283208257732753 ) ) ;
#23402=CARTESIAN_POINT ( 'NONE',  ( 68.13393739769618662, -1.666188944679350081, -65.65000000000000568 ) ) ;
#23408=CARTESIAN_POINT ( 'NONE',  ( 68.13393739769598767, -2.032350560840590070, -29.09832030244560741 ) ) ;
#23431=FACE_BOUND ( 'NONE', #4622, .T. ) ;
#23475=CARTESIAN_POINT ( 'NONE',  ( 68.13393739769618662, 0.9838110553206419473, -51.14999999999999858 ) ) ;
#23533=LINE ( 'NONE', #19875, #49512 ) ;
#23546=AXIS2_PLACEMENT_3D ( 'NONE', #17957, #26327, #49942 ) ;
#23644=DIRECTION ( 'NONE',  ( -1.000000000000000000, 0.000000000000000000, 0.000000000000000000 ) ) ;
#23662=DIRECTION ( 'NONE',  ( -1.000000000000000000, 0.000000000000000000, 0.000000000000000000 ) ) ;
#23681=AXIS2_PLACEMENT_3D ( 'NONE', #2950, #18920, #11335 ) ;
#23704=CARTESIAN_POINT ( 'NONE',  ( 68.13393739769618662, -0.5161889446793590519, -65.65000000000000568 ) ) ;
#23753=DIRECTION ( 'NONE',  ( 0.000000000000000000, 1.000000000000000000, 0.000000000000000000 ) ) ;
#23761=ADVANCED_FACE ( 'NONE', ( #14835 ), #8606, .T. ) ;
#23775=DIRECTION ( 'NONE',  ( 0.000000000000000000, -1.000000000000000000, 0.000000000000000000 ) ) ;
#23796=EDGE_CURVE ( 'NONE', #48087, #29490, #42093, .T. ) ;
#23837=( LENGTH_UNIT ( ) NAMED_UNIT ( * ) SI_UNIT ( .MILLI., .METRE. ) );
#23889=CIRCLE ( 'NONE', #39822, 0.5000000000814214252 ) ;
#23916=CARTESIAN_POINT ( 'NONE',  ( 104.6856170952499951, -2.032350560839819131, -29.09832030244561807 ) ) ;
#23983=CARTESIAN_POINT ( 'NONE',  ( 67.48834183618497207, -25.01418894467940035, -66.11905263132939581 ) ) ;
#24013=DIRECTION ( 'NONE',  ( 8.409939412270706254E-12, -1.000000000000000000, 0.000000000000000000 ) ) ;
#24140=CIRCLE ( 'NONE', #33371, 1.500000000000001332 ) ;
#24170=FACE_OUTER_BOUND ( 'NONE', #16120, .T. ) ;
#24184=ORIENTED_EDGE ( 'NONE', *, *, #6924, .T. ) ;
#24229=VERTEX_POINT ( 'NONE', #7672 ) ;
#24253=CIRCLE ( 'NONE', #20907, 16.50000000000000000 ) ;
#24322=DIRECTION ( 'NONE',  ( 1.000000000000000000, 0.000000000000000000, 0.000000000000000000 ) ) ;
#24323=EDGE_LOOP ( 'NONE', ( #36450, #27984, #7627, #44855, #45054 ) ) ;
#24398=CARTESIAN_POINT ( 'NONE',  ( 62.03393739769618520, -30.31618894467939995, -65.65000000000000568 ) ) ;
#24404=TOROIDAL_SURFACE ( 'NONE', #43702, 25.00000000000000000, 1.000000000000000000 ) ;
#24406=EDGE_CURVE ( 'NONE', #24462, #15604, #32071, .T. ) ;
#24408=DIRECTION ( 'NONE',  ( 2.448986521869468475E-28, 2.813979115193090436E-11, -1.000000000000000000 ) ) ;
#24462=VERTEX_POINT ( 'NONE', #41889 ) ;
#24467=EDGE_CURVE ( 'NONE', #37382, #26336, #39630, .T. ) ;
#24474=EDGE_LOOP ( 'NONE', ( #7992, #50599 ) ) ;
#24489=ORIENTED_EDGE ( 'NONE', *, *, #6927, .F. ) ;
#24510=AXIS2_PLACEMENT_3D ( 'NONE', #16746, #48994, #9912 ) ;
#24584=VECTOR ( 'NONE', #407, 1000.000000000000000 ) ;
#24629=CARTESIAN_POINT ( 'NONE',  ( 68.13393739769618662, -30.31618894467939995, -65.65000000000000568 ) ) ;
#24704=ORIENTED_EDGE ( 'NONE', *, *, #35968, .F. ) ;
#24788=DIRECTION ( 'NONE',  ( 0.000000000000000000, 0.000000000000000000, 1.000000000000000000 ) ) ;
#24809=TOROIDAL_SURFACE ( 'NONE', #13959, 23.49999999832119713, 0.5000000000814219803 ) ;
#24812=EDGE_CURVE ( 'NONE', #14727, #29730, #22351, .T. ) ;
#24838=DIRECTION ( 'NONE',  ( -1.000000000000000000, 0.000000000000000000, 0.000000000000000000 ) ) ;
#24866=DIRECTION ( 'NONE',  ( 1.000000000000000000, 1.681650659181820415E-11, -1.224643064585135000E-16 ) ) ;
#24927=CARTESIAN_POINT ( 'NONE',  ( 68.13393739771808555, -29.66618894502720138, -65.65000000100739896 ) ) ;
#24932=ORIENTED_EDGE ( 'NONE', *, *, #11423, .T. ) ;
#25023=ORIENTED_EDGE ( 'NONE', *, *, #46144, .T. ) ;
#25044=CARTESIAN_POINT ( 'NONE',  ( 68.13393739769618662, -30.31618894467939995, -80.15000000000000568 ) ) ;
#25054=CARTESIAN_POINT ( 'NONE',  ( 68.13393739824140027, -1.666188945520784337, -49.15000000187050233 ) ) ;
#25056=DIRECTION ( 'NONE',  ( 0.000000000000000000, -1.000000000000000000, 0.000000000000000000 ) ) ;
#25061=EDGE_CURVE ( 'NONE', #1527, #29389, #12891, .T. ) ;
#25245=AXIS2_PLACEMENT_3D ( 'NONE', #1996, #10381, #9608 ) ;
#25327=DIRECTION ( 'NONE',  ( 0.000000000000000000, 0.000000000000000000, -1.000000000000000000 ) ) ;
#25400=ADVANCED_FACE ( 'NONE', ( #27883 ), #28394, .F. ) ;
#25549=ORIENTED_EDGE ( 'NONE', *, *, #17863, .T. ) ;
#25649=CARTESIAN_POINT ( 'NONE',  ( 31.58225770014180256, -2.032350560840031406, -102.2016796975540274 ) ) ;
#25686=VERTEX_POINT ( 'NONE', #29378 ) ;
#25708=DIRECTION ( 'NONE',  ( 0.000000000000000000, -1.000000000000000000, 0.000000000000000000 ) ) ;
#25723=AXIS2_PLACEMENT_3D ( 'NONE', #29843, #6023, #37217 ) ;
#25848=ORIENTED_EDGE ( 'NONE', *, *, #16036, .F. ) ;
#25849=DIRECTION ( 'NONE',  ( 0.000000000000000000, 0.000000000000000000, -1.000000000000000000 ) ) ;
#25903=CARTESIAN_POINT ( 'NONE',  ( 31.58225770014180256, -2.032350560841368114, -29.09832030244561807 ) ) ;
#25907=AXIS2_PLACEMENT_3D ( 'NONE', #23160, #12420, #27364 ) ;
#25916=ORIENTED_EDGE ( 'NONE', *, *, #30272, .F. ) ;
#25954=VECTOR ( 'NONE', #36572, 1000.000000000000114 ) ;
#25957=CIRCLE ( 'NONE', #2560, 34.55616290057869833 ) ;
#25990=CARTESIAN_POINT ( 'NONE',  ( 68.13393739769618662, -30.31618894467939995, -65.65000000000000568 ) ) ;
#26032=TOROIDAL_SURFACE ( 'NONE', #36101, 23.49999999832119713, 0.5000000000814219803 ) ;
#26056=ADVANCED_FACE ( 'NONE', ( #23431, #32320 ), #43895, .T. ) ;
#26067=DIRECTION ( 'NONE',  ( -1.000000000000000000, -0.000000000000000000, -0.000000000000000000 ) ) ;
#26169=CARTESIAN_POINT ( 'NONE',  ( 104.6856170952499809, -2.032350560839140119, -65.65000000000000568 ) ) ;
#26191=EDGE_CURVE ( 'NONE', #31099, #34663, #38671, .T. ) ;
#26237=CARTESIAN_POINT ( 'NONE',  ( 52.13393739769618662, -1.166188944679350081, -65.65000000000000568 ) ) ;
#26323=EDGE_LOOP ( 'NONE', ( #29381, #26847, #43821, #43377 ) ) ;
#26327=DIRECTION ( 'NONE',  ( 1.964275807512749840E-11, -1.000000000000000000, -5.103645611290830066E-11 ) ) ;
#26336=VERTEX_POINT ( 'NONE', #12105 ) ;
#26523=CIRCLE ( 'NONE', #7277, 1.000000000000000888 ) ;
#26546=CARTESIAN_POINT ( 'NONE',  ( 0.000000000000000000, 0.000000000000000000, 0.000000000000000000 ) ) ;
#26555=MECHANICAL_DESIGN_GEOMETRIC_PRESENTATION_REPRESENTATION('',(#32375),#39122);
#26593=DIRECTION ( 'NONE',  ( 1.000000000000000000, 0.000000000000000000, 0.000000000000000000 ) ) ;
#26711=EDGE_CURVE ( 'NONE', #34663, #25686, #35725, .T. ) ;
#26737=CYLINDRICAL_SURFACE ( 'NONE', #49782, 16.00000000000000000 ) ;
#26762=DIRECTION ( 'NONE',  ( -1.000000000000000000, 0.000000000000000000, 0.000000000000000000 ) ) ;
#26792=ORIENTED_EDGE ( 'NONE', *, *, #15909, .T. ) ;
#26817=AXIS2_PLACEMENT_3D ( 'NONE', #20879, #40293, #24013 ) ;
#26822=CLOSED_SHELL ( 'NONE', ( #50283, #35053, #32791, #7406, #32201, #35946, #1826, #31457, #17743, #21638, #37154, #39328, #27267, #38463, #8800, #21755, #20971, #32546, #26056, #30161, #40326, #32043, #11295, #17321, #32854, #1759, #35238, #35826, #49633, #50865, #19076, #23761, #19850, #31168, #8236, #7570, #25400, #6274 ) ) ;
#26847=ORIENTED_EDGE ( 'NONE', *, *, #43444, .T. ) ;
#26890=AXIS2_PLACEMENT_3D ( 'NONE', #45287, #9128, #48441 ) ;
#26911=FACE_OUTER_BOUND ( 'NONE', #50728, .T. ) ;
#26960=DIRECTION ( 'NONE',  ( 0.000000000000000000, -1.000000000000000000, 0.000000000000000000 ) ) ;
#26992=EDGE_LOOP ( 'NONE', ( #28200, #16162, #36206, #36050, #41075, #7954 ) ) ;
#27008=ORIENTED_EDGE ( 'NONE', *, *, #49823, .F. ) ;
#27034=DIRECTION ( 'NONE',  ( 0.000000000000000000, -1.000000000000000000, 0.000000000000000000 ) ) ;
#27054=VERTEX_POINT ( 'NONE', #30755 ) ;
#27164=CARTESIAN_POINT ( 'NONE',  ( 68.13393739844677555, -29.16618894467940137, -42.14999999999999858 ) ) ;
#27236=DIRECTION ( 'NONE',  ( -1.000000000000000000, 0.000000000000000000, 0.000000000000000000 ) ) ;
#27267=ADVANCED_FACE ( 'NONE', ( #35978 ), #24809, .F. ) ;
#27364=DIRECTION ( 'NONE',  ( 0.000000000000000000, 0.000000000000000000, -1.000000000000000000 ) ) ;
#27373=EDGE_CURVE ( 'NONE', #47321, #37740, #6448, .T. ) ;
#27387=ORIENTED_EDGE ( 'NONE', *, *, #27774, .T. ) ;
#27435=EDGE_CURVE ( 'NONE', #14727, #42029, #23135, .T. ) ;
#27515=DIRECTION ( 'NONE',  ( -0.5720614028176880250, 0.7071067811865480168, 0.4156269377774474139 ) ) ;
#27572=EDGE_LOOP ( 'NONE', ( #10603, #49797, #48127, #40979 ) ) ;
#27605=LINE ( 'NONE', #102, #16157 ) ;
#27613=CARTESIAN_POINT ( 'NONE',  ( 68.13393739769625768, -15.41618894467990764, -28.20067248431510976 ) ) ;
#27674=CARTESIAN_POINT ( 'NONE',  ( 68.13393739769618662, -0.5161889446793590519, -65.65000000000000568 ) ) ;
#27701=FACE_OUTER_BOUND ( 'NONE', #9726, .T. ) ;
#27719=DIRECTION ( 'NONE',  ( 1.000000000000000000, 0.000000000000000000, -1.224646799147353207E-16 ) ) ;
#27758=DIRECTION ( 'NONE',  ( 0.000000000000000000, -1.000000000000000000, 0.000000000000000000 ) ) ;
#27774=EDGE_CURVE ( 'NONE', #29389, #15078, #22240, .T. ) ;
#27776=EDGE_CURVE ( 'NONE', #1527, #13981, #51557, .T. ) ;
#27779=PRODUCT_CONTEXT ( 'NONE', #19408, 'mechanical' ) ;
#27825=VERTEX_POINT ( 'NONE', #16011 ) ;
#27868=CARTESIAN_POINT ( 'NONE',  ( 104.6856170952499951, -2.032350560838469100, -102.2016796975540274 ) ) ;
#27880=AXIS2_PLACEMENT_3D ( 'NONE', #12586, #37205, #13120 ) ;
#27883=FACE_OUTER_BOUND ( 'NONE', #33678, .T. ) ;
#27896=AXIS2_PLACEMENT_3D ( 'NONE', #17273, #41113, #49507 ) ;
#27959=AXIS2_PLACEMENT_3D ( 'NONE', #39311, #34321, #42735 ) ;
#27984=ORIENTED_EDGE ( 'NONE', *, *, #13717, .T. ) ;
#28077=EDGE_LOOP ( 'NONE', ( #40465, #10020 ) ) ;
#28119=CARTESIAN_POINT ( 'NONE',  ( 31.58225770014180256, -2.032350560841368114, -29.09832030244561807 ) ) ;
#28200=ORIENTED_EDGE ( 'NONE', *, *, #19116, .F. ) ;
#28232=AXIS2_PLACEMENT_3D ( 'NONE', #19831, #11985, #16672 ) ;
#28253=ORIENTED_EDGE ( 'NONE', *, *, #2527, .F. ) ;
#28303=AXIS2_PLACEMENT_3D ( 'NONE', #30078, #29815, #18557 ) ;
#28323=EDGE_CURVE ( 'NONE', #25686, #31172, #44035, .T. ) ;
#28355=VERTEX_POINT ( 'NONE', #1970 ) ;
#28394=CYLINDRICAL_SURFACE ( 'NONE', #5955, 6.099999999999994316 ) ;
#28402=DIRECTION ( 'NONE',  ( -0.000000000000000000, 1.000000000000000000, 0.000000000000000000 ) ) ;
#28555=EDGE_CURVE ( 'NONE', #6777, #43941, #5560, .T. ) ;
#28596=EDGE_LOOP ( 'NONE', ( #1602, #23225 ) ) ;
#28623=CIRCLE ( 'NONE', #40462, 6.099999999999994316 ) ;
#28663=VERTEX_POINT ( 'NONE', #50581 ) ;
#28736=CIRCLE ( 'NONE', #38794, 16.00000000000000000 ) ;
#28745=DIRECTION ( 'NONE',  ( -1.000000000000000000, 0.000000000000000000, 0.000000000000000000 ) ) ;
#28843=DIRECTION ( 'NONE',  ( 1.000000000000000000, 0.000000000000000000, -1.224646799147353207E-16 ) ) ;
#28881=CIRCLE ( 'NONE', #46507, 0.5000000000336679573 ) ;
#28919=VERTEX_POINT ( 'NONE', #32171 ) ;
#28976=EDGE_LOOP ( 'NONE', ( #45871, #24932, #18573, #26792, #16831 ) ) ;
#29015=DIRECTION ( 'NONE',  ( 0.000000000000000000, -1.000000000000000000, 0.000000000000000000 ) ) ;
#29081=DIRECTION ( 'NONE',  ( 0.000000000000000000, 0.000000000000000000, -1.000000000000000000 ) ) ;
#29192=EDGE_CURVE ( 'NONE', #28663, #28355, #13045, .T. ) ;
#29219=VERTEX_POINT ( 'NONE', #50520 ) ;
#29230=ORIENTED_EDGE ( 'NONE', *, *, #23796, .T. ) ;
#29280=CIRCLE ( 'NONE', #30145, 2.000000000000001776 ) ;
#29283=VERTEX_POINT ( 'NONE', #22453 ) ;
#29305=CARTESIAN_POINT ( 'NONE',  ( 68.13393739769618662, -0.3411889446793609504, -65.65000000000000568 ) ) ;
#29378=CARTESIAN_POINT ( 'NONE',  ( 84.13393739769618662, -1.166188944679350081, -65.65000000000000568 ) ) ;
#29381=ORIENTED_EDGE ( 'NONE', *, *, #51305, .F. ) ;
#29389=VERTEX_POINT ( 'NONE', #33987 ) ;
#29490=VERTEX_POINT ( 'NONE', #47370 ) ;
#29683=ORIENTED_EDGE ( 'NONE', *, *, #34222, .T. ) ;
#29730=VERTEX_POINT ( 'NONE', #26237 ) ;
#29774=DIRECTION ( 'NONE',  ( 0.000000000000000000, -1.000000000000000000, 0.000000000000000000 ) ) ;
#29804=CARTESIAN_POINT ( 'NONE',  ( 68.13393739769618662, -0.1661889446793599900, -65.65000000000000568 ) ) ;
#29815=DIRECTION ( 'NONE',  ( 0.000000000000000000, 1.000000000000000000, 0.000000000000000000 ) ) ;
#29838=CARTESIAN_POINT ( 'NONE',  ( 31.58225770014201572, -28.80002732851900049, -102.2016796975550079 ) ) ;
#29843=CARTESIAN_POINT ( 'NONE',  ( 68.13393739845098196, -29.66618894499051962, -89.14999999951589871 ) ) ;
#29941=DIRECTION ( 'NONE',  ( 1.147431558122957675E-27, 2.220771714818679968E-11, -1.000000000000000000 ) ) ;
#30078=CARTESIAN_POINT ( 'NONE',  ( 68.13393739769618662, -29.66618894467940137, -65.65000000000000568 ) ) ;
#30145=AXIS2_PLACEMENT_3D ( 'NONE', #10903, #19781, #14567 ) ;
#30161=ADVANCED_FACE ( 'NONE', ( #16183, #12787 ), #20359, .T. ) ;
#30168=CIRCLE ( 'NONE', #45222, 25.00000000000000000 ) ;
#30203=DIRECTION ( 'NONE',  ( 0.000000000000000000, -1.000000000000000000, 0.000000000000000000 ) ) ;
#30214=DIRECTION ( 'NONE',  ( 0.000000000000000000, -1.000000000000000000, 0.000000000000000000 ) ) ;
#30272=EDGE_CURVE ( 'NONE', #15078, #29389, #30168, .T. ) ;
#30311=CARTESIAN_POINT ( 'NONE',  ( 68.13393739769618662, -2.166188944679360073, -65.65000000000000568 ) ) ;
#30357=CARTESIAN_POINT ( 'NONE',  ( 104.6856170952509757, -28.80002732851738045, -102.2016796975550079 ) ) ;
#30443=DIRECTION ( 'NONE',  ( -1.000000000000000000, 0.000000000000000000, 0.000000000000000000 ) ) ;
#30617=CARTESIAN_POINT ( 'NONE',  ( 31.58225770014201572, -28.80002732852027947, -29.09832030244561807 ) ) ;
#30663=CARTESIAN_POINT ( 'NONE',  ( 68.13393739769618662, -2.032350560841069687, -65.65000000000000568 ) ) ;
#30755=CARTESIAN_POINT ( 'NONE',  ( 74.23393739769618094, -0.5161889446793590519, -65.65000000000000568 ) ) ;
#30789=APPLICATION_CONTEXT ( 'automotive_design' ) ;
#30797=DIRECTION ( 'NONE',  ( 0.000000000000000000, 0.000000000000000000, -1.000000000000000000 ) ) ;
#30830=DIRECTION ( 'NONE',  ( 0.000000000000000000, 0.000000000000000000, -1.000000000000000000 ) ) ;
#30917=CARTESIAN_POINT ( 'NONE',  ( 68.13393739806289773, -1.666188944679350081, -89.15000000000000568 ) ) ;
#30951=DIRECTION ( 'NONE',  ( -1.000000000000000000, 0.000000000000000000, 0.000000000000000000 ) ) ;
#30963=VECTOR ( 'NONE', #49416, 1000.000000000000000 ) ;
#30978=CARTESIAN_POINT ( 'NONE',  ( 68.13393739845098196, -29.66618894551239904, -65.65000000119469803 ) ) ;
#31026=EDGE_CURVE ( 'NONE', #26336, #37382, #34480, .T. ) ;
#31099=VERTEX_POINT ( 'NONE', #40422 ) ;
#31137=DIRECTION ( 'NONE',  ( 0.000000000000000000, 0.000000000000000000, -1.000000000000000000 ) ) ;
#31168=ADVANCED_FACE ( 'NONE', ( #14907 ), #16014, .F. ) ;
#31172=VERTEX_POINT ( 'NONE', #2864 ) ;
#31179=ORIENTED_EDGE ( 'NONE', *, *, #35968, .T. ) ;
#31252=AXIS2_PLACEMENT_3D ( 'NONE', #202, #32396, #31631 ) ;
#31315=AXIS2_PLACEMENT_3D ( 'NONE', #48693, #29015, #37150 ) ;
#31341=CARTESIAN_POINT ( 'NONE',  ( 68.13393739769618662, -30.66618894467940137, -100.2061629005786898 ) ) ;
#31357=AXIS2_PLACEMENT_3D ( 'NONE', #47151, #27719, #47408 ) ;
#31404=CARTESIAN_POINT ( 'NONE',  ( 68.13393739769618662, -25.01418894467940035, -65.65000000000000568 ) ) ;
#31457=ADVANCED_FACE ( 'NONE', ( #48959 ), #2050, .T. ) ;
#31487=PRODUCT_DEFINITION ( 'UNKNOWN', '', #49473, #39983 ) ;
#31522=CARTESIAN_POINT ( 'NONE',  ( 68.13393739769618662, -31.81618894467930403, -65.65000000000000568 ) ) ;
#31538=DIRECTION ( 'NONE',  ( -1.000000000000000000, 0.000000000000000000, 0.000000000000000000 ) ) ;
#31552=CARTESIAN_POINT ( 'NONE',  ( 68.13393739769618662, -30.66618894467940137, -65.65000000000000568 ) ) ;
#31559=DIRECTION ( 'NONE',  ( 0.000000000000000000, 0.000000000000000000, 1.000000000000000000 ) ) ;
#31584=CARTESIAN_POINT ( 'NONE',  ( 73.06894106338339157, -30.31618894467939995, -62.06450996101596473 ) ) ;
#31603=ORIENTED_EDGE ( 'NONE', *, *, #5517, .F. ) ;
#31631=DIRECTION ( 'NONE',  ( 0.000000000000000000, 0.000000000000000000, 1.000000000000000000 ) ) ;
#31683=DIRECTION ( 'NONE',  ( 1.000000000000000000, 1.964275807512750486E-11, -1.224636774179748846E-16 ) ) ;
#31699=AXIS2_PLACEMENT_3D ( 'NONE', #13129, #45075, #9184 ) ;
#31732=ORIENTED_EDGE ( 'NONE', *, *, #2844, .T. ) ;
#31790=CARTESIAN_POINT ( 'NONE',  ( 105.5832649133809724, -15.41618894467840484, -65.65000000000004832 ) ) ;
#31869=EDGE_LOOP ( 'NONE', ( #36438, #49513 ) ) ;
#31884=CARTESIAN_POINT ( 'NONE',  ( 52.13393739769618662, -0.5161889446793590519, -65.65000000000000568 ) ) ;
#31920=ORIENTED_EDGE ( 'NONE', *, *, #16653, .T. ) ;
#31931=VERTEX_POINT ( 'NONE', #24398 ) ;
#31971=ORIENTED_EDGE ( 'NONE', *, *, #1888, .T. ) ;
#31982=ORIENTED_EDGE ( 'NONE', *, *, #6927, .T. ) ;
#32041=CARTESIAN_POINT ( 'NONE',  ( 31.58225770014178835, -2.032350560840699760, -65.65000000000000568 ) ) ;
#32043=ADVANCED_FACE ( 'NONE', ( #39585, #35121 ), #3690, .T. ) ;
#32068=TOROIDAL_SURFACE ( 'NONE', #50506, 34.55616290057869833, 2.000000000000000000 ) ;
#32071=CIRCLE ( 'NONE', #27896, 6.099999999999994316 ) ;
#32093=PLANE ( 'NONE',  #22097 ) ;
#32123=AXIS2_PLACEMENT_3D ( 'NONE', #38886, #14508, #6396 ) ;
#32135=TOROIDAL_SURFACE ( 'NONE', #27959, 34.55616290057869833, 2.000000000000000000 ) ;
#32171=CARTESIAN_POINT ( 'NONE',  ( 68.13393739769618662, -2.032350560841069687, -102.2016796975542690 ) ) ;
#32201=ADVANCED_FACE ( 'NONE', ( #16177 ), #7101, .T. ) ;
#32260=( LENGTH_UNIT ( ) NAMED_UNIT ( * ) SI_UNIT ( .MILLI., .METRE. ) );
#32279=CARTESIAN_POINT ( 'NONE',  ( 74.28246655494581319, 0.9838110553206419473, -70.11716791742273358 ) ) ;
#32280=DIRECTION ( 'NONE',  ( 1.147431558122957675E-27, 2.220771714818679968E-11, -1.000000000000000000 ) ) ;
#32307=AXIS2_PLACEMENT_3D ( 'NONE', #29305, #17274, #7927 ) ;
#32309=EDGE_CURVE ( 'NONE', #29219, #17717, #28623, .T. ) ;
#32320=FACE_OUTER_BOUND ( 'NONE', #17201, .T. ) ;
#32375=STYLED_ITEM ( 'NONE', ( #17047 ), #43885 ) ;
#32381=DIRECTION ( 'NONE',  ( -1.000000000000000000, 0.000000000000000000, 0.000000000000000000 ) ) ;
#32396=DIRECTION ( 'NONE',  ( -1.000000000000000000, -0.000000000000000000, -0.000000000000000000 ) ) ;
#32455=FACE_BOUND ( 'NONE', #44268, .T. ) ;
#32513=VERTEX_POINT ( 'NONE', #49017 ) ;
#32546=ADVANCED_FACE ( 'NONE', ( #32455, #1043 ), #40874, .T. ) ;
#32553=DIRECTION ( 'NONE',  ( -1.000000000000000000, 0.000000000000000000, 0.000000000000000000 ) ) ;
#32556=CONICAL_SURFACE ( 'NONE', #39298, 0.7980000000000000426, 0.7853981633974476129 ) ;
#32577=ORIENTED_EDGE ( 'NONE', *, *, #42880, .F. ) ;
#32644=ORIENTED_EDGE ( 'NONE', *, *, #43080, .F. ) ;
#32656=DIRECTION ( 'NONE',  ( 0.000000000000000000, 1.000000000000000000, 0.000000000000000000 ) ) ;
#32720=FACE_OUTER_BOUND ( 'NONE', #22701, .T. ) ;
#32728=DIRECTION ( 'NONE',  ( 0.000000000000000000, -1.000000000000000000, 0.000000000000000000 ) ) ;
#32741=CIRCLE ( 'NONE', #25245, 24.00000000000000000 ) ;
#32754=DIRECTION ( 'NONE',  ( 0.000000000000000000, -1.000000000000000000, 0.000000000000000000 ) ) ;
#32791=ADVANCED_FACE ( 'NONE', ( #38861 ), #51169, .F. ) ;
#32798=DIRECTION ( 'NONE',  ( 2.806155971274087206E-29, 5.103645611290830066E-11, -1.000000000000000000 ) ) ;
#32822=DIRECTION ( 'NONE',  ( 0.000000000000000000, -1.000000000000000000, 0.000000000000000000 ) ) ;
#32854=ADVANCED_FACE ( 'NONE', ( #4483 ), #1073, .T. ) ;
#32856=EDGE_LOOP ( 'NONE', ( #32577, #19953, #41959, #27387 ) ) ;
#32903=DIRECTION ( 'NONE',  ( 0.000000000000000000, -1.000000000000000000, 0.000000000000000000 ) ) ;
#32975=CARTESIAN_POINT ( 'NONE',  ( 68.13393739806078031, -1.166188945451896330, -42.15000000163579585 ) ) ;
#32996=CARTESIAN_POINT ( 'NONE',  ( 68.13393739845098196, -29.66618894603428203, -42.15000000287349735 ) ) ;
#33102=ORIENTED_EDGE ( 'NONE', *, *, #2403, .T. ) ;
#33158=ORIENTED_EDGE ( 'NONE', *, *, #19351, .T. ) ;
#33163=EDGE_CURVE ( 'NONE', #40265, #7973, #42946, .T. ) ;
#33164=ORIENTED_EDGE ( 'NONE', *, *, #1490, .T. ) ;
#33212=CARTESIAN_POINT ( 'NONE',  ( 68.13393739769618662, -29.16618894467940137, -65.65000000000000568 ) ) ;
#33227=EDGE_CURVE ( 'NONE', #6636, #27825, #37082, .T. ) ;
#33302=EDGE_LOOP ( 'NONE', ( #24489, #10783, #41553, #38847, #16400, #6825 ) ) ;
#33359=ORIENTED_EDGE ( 'NONE', *, *, #44674, .T. ) ;
#33371=AXIS2_PLACEMENT_3D ( 'NONE', #42564, #37849, #13998 ) ;
#33373=CONICAL_SURFACE ( 'NONE', #14974, 0.7980000000000000426, 0.7853981633974476129 ) ;
#33376=DIRECTION ( 'NONE',  ( 0.000000000000000000, 1.000000000000000000, 0.000000000000000000 ) ) ;
#33435=AXIS2_PLACEMENT_3D ( 'NONE', #41969, #31683, #23055 ) ;
#33483=ORIENTED_EDGE ( 'NONE', *, *, #45012, .T. ) ;
#33678=EDGE_LOOP ( 'NONE', ( #40208, #413, #7988, #50603, #43892, #18961 ) ) ;
#33712=PLANE ( 'NONE',  #48159 ) ;
#33913=EDGE_CURVE ( 'NONE', #31172, #29730, #28736, .T. ) ;
#33987=CARTESIAN_POINT ( 'NONE',  ( 68.13393739769618662, -0.1661889446793515246, -90.65000000000000568 ) ) ;
#34030=CARTESIAN_POINT ( 'NONE',  ( 68.13393739769625768, -15.41618894467990764, -28.20067248431510976 ) ) ;
#34070=CARTESIAN_POINT ( 'NONE',  ( 68.13393739769618662, -5.818188944679350882, -65.65000000000000568 ) ) ;
#34074=ORIENTED_EDGE ( 'NONE', *, *, #1960, .F. ) ;
#34106=AXIS2_PLACEMENT_3D ( 'NONE', #30663, #9989, #42750 ) ;
#34130=FACE_OUTER_BOUND ( 'NONE', #5407, .T. ) ;
#34197=EDGE_LOOP ( 'NONE', ( #19570, #20324, #10958, #11760, #7335 ) ) ;
#34214=CARTESIAN_POINT ( 'NONE',  ( 62.03393739769618520, -15.41618894467939782, -65.65000000000000568 ) ) ;
#34222=EDGE_CURVE ( 'NONE', #27054, #29219, #22898, .T. ) ;
#34274=CARTESIAN_POINT ( 'NONE',  ( 68.13393739771647972, -29.16618894506861892, -49.15000000085210274 ) ) ;
#34315=ORIENTED_EDGE ( 'NONE', *, *, #16036, .T. ) ;
#34321=DIRECTION ( 'NONE',  ( 0.000000000000000000, -1.000000000000000000, 0.000000000000000000 ) ) ;
#34364=DIRECTION ( 'NONE',  ( 0.000000000000000000, -1.000000000000000000, 0.000000000000000000 ) ) ;
#34480=CIRCLE ( 'NONE', #11924, 14.49999999999999822 ) ;
#34663=VERTEX_POINT ( 'NONE', #40594 ) ;
#34695=DIRECTION ( 'NONE',  ( 1.000000000000000000, 0.000000000000000000, 0.000000000000000000 ) ) ;
#34725=CARTESIAN_POINT ( 'NONE',  ( 68.13393739769618662, -28.66618894467939782, -100.2061629005786898 ) ) ;
#34894=CARTESIAN_POINT ( 'NONE',  ( 68.13393739769618662, -29.16618894467940137, -65.65000000000000568 ) ) ;
#34905=DIRECTION ( 'NONE',  ( -1.000000000000000000, -1.964275807512749840E-11, -1.002496760437719626E-21 ) ) ;
#34958=CARTESIAN_POINT ( 'NONE',  ( 68.13393739769658453, -28.80002732851960445, -29.09832030244560741 ) ) ;
#35053=ADVANCED_FACE ( 'NONE', ( #27701 ), #15403, .F. ) ;
#35076=EDGE_CURVE ( 'NONE', #14944, #17025, #19613, .T. ) ;
#35087=AXIS2_PLACEMENT_3D ( 'NONE', #5450, #1765, #41336 ) ;
#35107=DIRECTION ( 'NONE',  ( 0.000000000000000000, -1.000000000000000000, 0.000000000000000000 ) ) ;
#35121=FACE_OUTER_BOUND ( 'NONE', #28596, .T. ) ;
#35204=AXIS2_PLACEMENT_3D ( 'NONE', #50289, #2321, #14376 ) ;
#35238=ADVANCED_FACE ( 'NONE', ( #42560 ), #42230, .F. ) ;
#35273=TOROIDAL_SURFACE ( 'NONE', #10185, 25.00000000000000000, 1.000000000000000000 ) ;
#35275=CIRCLE ( 'NONE', #47857, 16.00000000000000000 ) ;
#35294=DIRECTION ( 'NONE',  ( 0.000000000000000000, -1.000000000000000000, 0.000000000000000000 ) ) ;
#35301=DIRECTION ( 'NONE',  ( 1.000000000000000000, 0.000000000000000000, 0.000000000000000000 ) ) ;
#35365=FACE_OUTER_BOUND ( 'NONE', #26323, .T. ) ;
#35440=ORIENTED_EDGE ( 'NONE', *, *, #12660, .F. ) ;
#35516=DIRECTION ( 'NONE',  ( -1.000000000000000000, -0.000000000000000000, -0.000000000000000000 ) ) ;
#35702=ORIENTED_EDGE ( 'NONE', *, *, #33163, .T. ) ;
#35725=CIRCLE ( 'NONE', #22314, 16.00000000000000000 ) ;
#35734=DIRECTION ( 'NONE',  ( 1.000000000000000000, 0.000000000000000000, 0.000000000000000000 ) ) ;
#35775=EDGE_LOOP ( 'NONE', ( #3601, #33164, #15634, #33483 ) ) ;
#35809=AXIS2_PLACEMENT_3D ( 'NONE', #35850, #23775, #16189 ) ;
#35826=ADVANCED_FACE ( 'NONE', ( #18627 ), #26737, .T. ) ;
#35850=CARTESIAN_POINT ( 'NONE',  ( 68.13393739769618662, -31.81618894467930403, -65.65000000000000568 ) ) ;
#35922=ORIENTED_EDGE ( 'NONE', *, *, #4774, .F. ) ;
#35946=ADVANCED_FACE ( 'NONE', ( #40096 ), #19658, .T. ) ;
#35951=AXIS2_PLACEMENT_3D ( 'NONE', #15179, #26960, #31137 ) ;
#35953=ORIENTED_EDGE ( 'NONE', *, *, #44674, .F. ) ;
#35962=AXIS2_PLACEMENT_3D ( 'NONE', #46011, #49939, #14546 ) ;
#35968=EDGE_CURVE ( 'NONE', #29219, #5979, #39840, .T. ) ;
#35978=FACE_OUTER_BOUND ( 'NONE', #45506, .T. ) ;
#35983=CIRCLE ( 'NONE', #13424, 23.50000000000000000 ) ;
#36008=DIRECTION ( 'NONE',  ( 0.000000000000000000, -1.000000000000000000, 0.000000000000000000 ) ) ;
#36050=ORIENTED_EDGE ( 'NONE', *, *, #33227, .T. ) ;
#36051=CIRCLE ( 'NONE', #38587, 1.500000000000001332 ) ;
#36057=TOROIDAL_SURFACE ( 'NONE', #35951, 25.00000000000000000, 1.000000000000000000 ) ;
#36101=AXIS2_PLACEMENT_3D ( 'NONE', #30978, #13984, #29941 ) ;
#36119=ORIENTED_EDGE ( 'NONE', *, *, #5945, .T. ) ;
#36155=CARTESIAN_POINT ( 'NONE',  ( 68.13393739769618662, -2.166188944679360073, -65.65000000000000568 ) ) ;
#36206=ORIENTED_EDGE ( 'NONE', *, *, #2613, .F. ) ;
#36274=EDGE_LOOP ( 'NONE', ( #16998, #511 ) ) ;
#36314=VERTEX_POINT ( 'NONE', #45518 ) ;
#36322=ORIENTED_EDGE ( 'NONE', *, *, #39214, .T. ) ;
#36359=AXIS2_PLACEMENT_3D ( 'NONE', #36155, #7360, #48218 ) ;
#36382=DIRECTION ( 'NONE',  ( -1.000000000000000000, 0.000000000000000000, 0.000000000000000000 ) ) ;
#36401=CIRCLE ( 'NONE', #50678, 23.50000000000000000 ) ;
#36438=ORIENTED_EDGE ( 'NONE', *, *, #27373, .F. ) ;
#36450=ORIENTED_EDGE ( 'NONE', *, *, #12770, .T. ) ;
#36453=CARTESIAN_POINT ( 'NONE',  ( 68.13393739769627189, -15.41618894467990586, -28.20067248431511331 ) ) ;
#36476=DIRECTION ( 'NONE',  ( 3.191443934968489902E-12, -1.000000000000000000, -2.813979115193090113E-11 ) ) ;
#36572=DIRECTION ( 'NONE',  ( -0.5720614028176880250, -0.7071067811865480168, -0.4156269377774474139 ) ) ;
#36588=CARTESIAN_POINT ( 'NONE',  ( 52.13393739769618662, -0.3411889446793609504, -65.65000000000000568 ) ) ;
#36920=EDGE_CURVE ( 'NONE', #44651, #51663, #36401, .T. ) ;
#37001=ORIENTED_EDGE ( 'NONE', *, *, #4468, .F. ) ;
#37082=LINE ( 'NONE', #37863, #51321 ) ;
#37111=ORIENTED_EDGE ( 'NONE', *, *, #33163, .F. ) ;
#37139=EDGE_CURVE ( 'NONE', #14944, #2360, #28881, .T. ) ;
#37141=DIRECTION ( 'NONE',  ( 1.000000000000000000, 0.000000000000000000, 0.000000000000000000 ) ) ;
#37150=DIRECTION ( 'NONE',  ( 0.000000000000000000, 0.000000000000000000, -1.000000000000000000 ) ) ;
#37154=ADVANCED_FACE ( 'NONE', ( #32720 ), #37982, .T. ) ;
#37161=ORIENTED_EDGE ( 'NONE', *, *, #24467, .T. ) ;
#37205=DIRECTION ( 'NONE',  ( -0.000000000000000000, 1.000000000000000000, 0.000000000000000000 ) ) ;
#37216=DIRECTION ( 'NONE',  ( 0.000000000000000000, -1.000000000000000000, 0.000000000000000000 ) ) ;
#37217=DIRECTION ( 'NONE',  ( 1.681987882033212302E-11, -1.000000000000000000, 0.000000000000000000 ) ) ;
#37324=EDGE_LOOP ( 'NONE', ( #47768, #996, #38432, #14812 ) ) ;
#37382=VERTEX_POINT ( 'NONE', #7060 ) ;
#37499=CIRCLE ( 'NONE', #25723, 0.5000000000814214252 ) ;
#37522=CARTESIAN_POINT ( 'NONE',  ( 68.13393739769618662, -0.5161889446793590519, -65.65000000000000568 ) ) ;
#37573=AXIS2_PLACEMENT_3D ( 'NONE', #27674, #48376, #44443 ) ;
#37613=CARTESIAN_POINT ( 'NONE',  ( 68.13393739771808555, -29.66618894549150909, -49.15000000170420691 ) ) ;
#37662=DIRECTION ( 'NONE',  ( -1.000000000000000000, 0.000000000000000000, 0.000000000000000000 ) ) ;
#37684=DIRECTION ( 'NONE',  ( -1.000000000000000000, 0.000000000000000000, 0.000000000000000000 ) ) ;
#37727=CARTESIAN_POINT ( 'NONE',  ( 68.13393739769598767, -2.032350560839250253, -102.2016796975539989 ) ) ;
#37740=VERTEX_POINT ( 'NONE', #45535 ) ;
#37779=LINE ( 'NONE', #9232, #49407 ) ;
#37804=CARTESIAN_POINT ( 'NONE',  ( 68.13393739769618662, -0.1661889446793529956, -65.65000000000000568 ) ) ;
#37849=DIRECTION ( 'NONE',  ( -1.000000000000000000, -0.000000000000000000, -0.000000000000000000 ) ) ;
#37863=CARTESIAN_POINT ( 'NONE',  ( 84.13393739769618662, -30.49118894467929763, -65.65000000000000568 ) ) ;
#37888=DIRECTION ( 'NONE',  ( 0.000000000000000000, 0.000000000000000000, 1.000000000000000000 ) ) ;
#37939=DIRECTION ( 'NONE',  ( 0.000000000000000000, -1.000000000000000000, 0.000000000000000000 ) ) ;
#37982=CYLINDRICAL_SURFACE ( 'NONE', #16364, 16.00000000000000000 ) ;
#38171=CARTESIAN_POINT ( 'NONE',  ( 68.13393739769618662, 0.9838110553206419473, -65.65000000000000568 ) ) ;
#38200=CARTESIAN_POINT ( 'NONE',  ( 68.13393739771727553, -29.66618894467940137, -49.64999999999999858 ) ) ;
#38205=ORIENTED_EDGE ( 'NONE', *, *, #19728, .T. ) ;
#38244=CARTESIAN_POINT ( 'NONE',  ( 68.13393739769658453, -28.80002732851960445, -29.09832030244560741 ) ) ;
#38267=ORIENTED_EDGE ( 'NONE', *, *, #5975, .F. ) ;
#38277=EDGE_CURVE ( 'NONE', #48161, #24229, #48236, .T. ) ;
#38368=( BOUNDED_CURVE ( )  B_SPLINE_CURVE ( 2, ( #5548, #36453, #12632 ),
 .UNSPECIFIED., .F., .T. ) 
 B_SPLINE_CURVE_WITH_KNOTS ( ( 3, 3 ),
 ( -0.06696923885014899325, 0.06696923885011449307 ),
 .UNSPECIFIED. ) 
 CURVE ( )  GEOMETRIC_REPRESENTATION_ITEM ( )  RATIONAL_B_SPLINE_CURVE ( ( 1.000000000000000000, 0.9977583984878120038, 1.000000000000000000 ) ) 
 REPRESENTATION_ITEM ( '' )  );
#38412=EDGE_LOOP ( 'NONE', ( #47331, #20282, #28253, #5214, #247, #31603 ) ) ;
#38432=ORIENTED_EDGE ( 'NONE', *, *, #14892, .T. ) ;
#38463=ADVANCED_FACE ( 'NONE', ( #4952 ), #5481, .T. ) ;
#38587=AXIS2_PLACEMENT_3D ( 'NONE', #40374, #286, #16270 ) ;
#38671=CIRCLE ( 'NONE', #16056, 0.4999999999096970127 ) ;
#38731=CARTESIAN_POINT ( 'NONE',  ( 68.13393739769618662, -30.66618894467940137, -65.65000000000000568 ) ) ;
#38772=CARTESIAN_POINT ( 'NONE',  ( 30.68460988201149320, -15.41618894467931611, -103.0993275156849762 ) ) ;
#38794=AXIS2_PLACEMENT_3D ( 'NONE', #19504, #37939, #31538 ) ;
#38806=CARTESIAN_POINT ( 'NONE',  ( 68.13393739769618662, -30.66618894467940137, -65.65000000000000568 ) ) ;
#38847=ORIENTED_EDGE ( 'NONE', *, *, #24406, .T. ) ;
#38861=FACE_OUTER_BOUND ( 'NONE', #33302, .T. ) ;
#38886=CARTESIAN_POINT ( 'NONE',  ( 68.13393739771808555, -29.66618894502720138, -65.65000000100739896 ) ) ;
#38900=ORIENTED_EDGE ( 'NONE', *, *, #10767, .F. ) ;
#39042=ORIENTED_EDGE ( 'NONE', *, *, #19728, .F. ) ;
#39122=( GEOMETRIC_REPRESENTATION_CONTEXT ( 3 ) GLOBAL_UNCERTAINTY_ASSIGNED_CONTEXT ( ( #8531 ) ) GLOBAL_UNIT_ASSIGNED_CONTEXT ( ( #23837, #1053, #47986 ) ) REPRESENTATION_CONTEXT ( 'NONE', 'WORKASPACE' ) );
#39214=EDGE_CURVE ( 'NONE', #43185, #28919, #20606, .T. ) ;
#39232=CARTESIAN_POINT ( 'NONE',  ( 52.13393739769618662, -29.66618894467940137, -65.65000000000000568 ) ) ;
#39247=VERTEX_POINT ( 'NONE', #13270 ) ;
#39252=DIRECTION ( 'NONE',  ( -1.000000000000000000, 0.000000000000000000, 0.000000000000000000 ) ) ;
#39298=AXIS2_PLACEMENT_3D ( 'NONE', #31404, #43489, #43743 ) ;
#39311=CARTESIAN_POINT ( 'NONE',  ( 68.13393739769618662, -28.66618894467939782, -65.65000000000000568 ) ) ;
#39328=ADVANCED_FACE ( 'NONE', ( #44878 ), #15621, .F. ) ;
#39393=EDGE_CURVE ( 'NONE', #42024, #15377, #40721, .T. ) ;
#39428=CARTESIAN_POINT ( 'NONE',  ( 105.5832649133809156, -15.41618894467769962, -103.0993275156849762 ) ) ;
#39517=ORIENTED_EDGE ( 'NONE', *, *, #5945, .F. ) ;
#39585=FACE_BOUND ( 'NONE', #24474, .T. ) ;
#39630=CIRCLE ( 'NONE', #24510, 14.49999999999999822 ) ;
#39822=AXIS2_PLACEMENT_3D ( 'NONE', #32996, #24866, #16253 ) ;
#39840=LINE ( 'NONE', #3689, #1253 ) ;
#39841=EDGE_CURVE ( 'NONE', #7973, #29283, #23889, .T. ) ;
#39889=AXIS2_PLACEMENT_3D ( 'NONE', #31522, #12150, #35734 ) ;
#39905=AXIS2_PLACEMENT_3D ( 'NONE', #25990, #50636, #30443 ) ;
#39941=CARTESIAN_POINT ( 'NONE',  ( 68.13393739769625768, -15.41618894467990764, -28.20067248431510976 ) ) ;
#39983=PRODUCT_DEFINITION_CONTEXT ( 'detailed design', #30789, 'design' ) ;
#40096=FACE_OUTER_BOUND ( 'NONE', #27572, .T. ) ;
#40101=DIRECTION ( 'NONE',  ( 0.000000000000000000, -1.000000000000000000, 0.000000000000000000 ) ) ;
#40194=CARTESIAN_POINT ( 'NONE',  ( 31.58225770014201572, -28.80002732851900049, -102.2016796975550079 ) ) ;
#40208=ORIENTED_EDGE ( 'NONE', *, *, #50470, .F. ) ;
#40251=EDGE_LOOP ( 'NONE', ( #37111, #39042 ) ) ;
#40265=VERTEX_POINT ( 'NONE', #45531 ) ;
#40293=DIRECTION ( 'NONE',  ( -1.000000000000000000, -8.402539340422011355E-12, -1.147202196707759143E-22 ) ) ;
#40326=ADVANCED_FACE ( 'NONE', ( #45271, #49726 ), #33712, .T. ) ;
#40374=CARTESIAN_POINT ( 'NONE',  ( 68.13393739769618662, -30.31618894467939995, -51.14999999999999858 ) ) ;
#40422=CARTESIAN_POINT ( 'NONE',  ( 68.13393739824141448, -1.666188944678682837, -82.14999999999919567 ) ) ;
#40430=AXIS2_PLACEMENT_3D ( 'NONE', #8476, #40435, #20246 ) ;
#40435=DIRECTION ( 'NONE',  ( 0.000000000000000000, -1.000000000000000000, 0.000000000000000000 ) ) ;
#40455=EDGE_LOOP ( 'NONE', ( #41131, #24184, #48073, #1997, #14375 ) ) ;
#40462=AXIS2_PLACEMENT_3D ( 'NONE', #37522, #49599, #16564 ) ;
#40465=ORIENTED_EDGE ( 'NONE', *, *, #29192, .F. ) ;
#40585=DIRECTION ( 'NONE',  ( 0.000000000000000000, -1.000000000000000000, 0.000000000000000000 ) ) ;
#40594=CARTESIAN_POINT ( 'NONE',  ( 68.13393739823651174, -1.166188944679350081, -81.65000000000000568 ) ) ;
#40721=CIRCLE ( 'NONE', #21469, 36.55167969755429880 ) ;
#40722=ORIENTED_EDGE ( 'NONE', *, *, #24406, .F. ) ;
#40813=EDGE_LOOP ( 'NONE', ( #4621, #7083, #6058, #42147 ) ) ;
#40874=PLANE ( 'NONE',  #27880 ) ;
#40948=DIRECTION ( 'NONE',  ( 1.964275807512749840E-11, -1.000000000000000000, -5.103645611290830066E-11 ) ) ;
#40979=ORIENTED_EDGE ( 'NONE', *, *, #39214, .F. ) ;
#41075=ORIENTED_EDGE ( 'NONE', *, *, #42242, .F. ) ;
#41113=DIRECTION ( 'NONE',  ( 0.000000000000000000, -1.000000000000000000, 0.000000000000000000 ) ) ;
#41131=ORIENTED_EDGE ( 'NONE', *, *, #13717, .F. ) ;
#41160=ORIENTED_EDGE ( 'NONE', *, *, #33913, .F. ) ;
#41189=DIRECTION ( 'NONE',  ( 1.000000000000000000, 0.000000000000000000, 0.000000000000000000 ) ) ;
#41311=ORIENTED_EDGE ( 'NONE', *, *, #1215, .T. ) ;
#41336=DIRECTION ( 'NONE',  ( -1.000000000000000000, 0.000000000000000000, 0.000000000000000000 ) ) ;
#41362=DIRECTION ( 'NONE',  ( 1.000000000000000000, 0.000000000000000000, 0.000000000000000000 ) ) ;
#41373=DIRECTION ( 'NONE',  ( -8.409939412270706254E-12, 1.000000000000000000, 0.000000000000000000 ) ) ;
#41440=DIRECTION ( 'NONE',  ( 0.000000000000000000, -1.000000000000000000, 0.000000000000000000 ) ) ;
#41527=DIRECTION ( 'NONE',  ( 0.000000000000000000, -1.000000000000000000, 0.000000000000000000 ) ) ;
#41548=CARTESIAN_POINT ( 'NONE',  ( 68.13393739769618662, -2.166188944679360073, -100.2061629005786898 ) ) ;
#41553=ORIENTED_EDGE ( 'NONE', *, *, #4774, .T. ) ;
#41738=DIRECTION ( 'NONE',  ( 1.000000000000000000, 0.000000000000000000, 0.000000000000000000 ) ) ;
#41764=CIRCLE ( 'NONE', #35087, 16.00000000000000000 ) ;
#41889=CARTESIAN_POINT ( 'NONE',  ( 63.19893373200898168, -30.31618894467939995, -69.23549003898403953 ) ) ;
#41918=CARTESIAN_POINT ( 'NONE',  ( 104.6856170952509757, -28.80002732851879088, -29.09832030244561807 ) ) ;
#41959=ORIENTED_EDGE ( 'NONE', *, *, #25061, .T. ) ;
#41969=CARTESIAN_POINT ( 'NONE',  ( 68.13393739823159478, -1.166188946452521469, -49.15000000374099898 ) ) ;
#41976=CARTESIAN_POINT ( 'NONE',  ( 68.13393739769618662, 0.9838110553206419473, -65.65000000000000568 ) ) ;
#42012=CARTESIAN_POINT ( 'NONE',  ( 68.13393739823159478, -1.166188944768318247, -82.14999999999838565 ) ) ;
#42024=VERTEX_POINT ( 'NONE', #12404 ) ;
#42029=VERTEX_POINT ( 'NONE', #16857 ) ;
#42043=( BOUNDED_CURVE ( )  B_SPLINE_CURVE ( 2, ( #16818, #4758, #17591 ),
 .UNSPECIFIED., .F., .T. ) 
 B_SPLINE_CURVE_WITH_KNOTS ( ( 3, 3 ),
 ( -0.06696923885014899325, 0.06696923885011449307 ),
 .UNSPECIFIED. ) 
 CURVE ( )  GEOMETRIC_REPRESENTATION_ITEM ( )  RATIONAL_B_SPLINE_CURVE ( ( 1.000000000000000000, 0.9977583984878120038, 1.000000000000000000 ) ) 
 REPRESENTATION_ITEM ( '' )  );
#42093=CIRCLE ( 'NONE', #20334, 14.49999999999999822 ) ;
#42145=CARTESIAN_POINT ( 'NONE',  ( 68.13393739806078031, -1.166188944679350081, -89.64999999988646096 ) ) ;
#42147=ORIENTED_EDGE ( 'NONE', *, *, #25061, .F. ) ;
#42179=CARTESIAN_POINT ( 'NONE',  ( 105.5832649133809156, -15.41618894467769962, -103.0993275156849762 ) ) ;
#42230=TOROIDAL_SURFACE ( 'NONE', #32123, 16.49999999930319916, 0.5000000000336690675 ) ;
#42242=EDGE_CURVE ( 'NONE', #43941, #27825, #3047, .T. ) ;
#42341=ORIENTED_EDGE ( 'NONE', *, *, #17349, .F. ) ;
#42346=ORIENTED_EDGE ( 'NONE', *, *, #15743, .F. ) ;
#42560=FACE_OUTER_BOUND ( 'NONE', #21373, .T. ) ;
#42564=CARTESIAN_POINT ( 'NONE',  ( 68.13393739769618662, -0.5161889446793590519, -80.15000000000000568 ) ) ;
#42584=CARTESIAN_POINT ( 'NONE',  ( 68.13393739769618662, -0.5161889446793590519, -65.65000000000000568 ) ) ;
#42630=LINE ( 'NONE', #34214, #47671 ) ;
#42660=DIRECTION ( 'NONE',  ( 0.000000000000000000, -1.000000000000000000, 0.000000000000000000 ) ) ;
#42703=CARTESIAN_POINT ( 'NONE',  ( 104.6856170952499951, -2.032350560838469100, -102.2016796975540274 ) ) ;
#42735=DIRECTION ( 'NONE',  ( 0.000000000000000000, 0.000000000000000000, -1.000000000000000000 ) ) ;
#42736=CARTESIAN_POINT ( 'NONE',  ( 68.13393739769618662, -1.166188944679350081, -65.65000000000000568 ) ) ;
#42750=DIRECTION ( 'NONE',  ( 1.000000000000000000, 0.000000000000000000, 0.000000000000000000 ) ) ;
#42776=DIRECTION ( 'NONE',  ( -1.000000000000000000, 0.000000000000000000, 0.000000000000000000 ) ) ;
#42865=ORIENTED_EDGE ( 'NONE', *, *, #2613, .T. ) ;
#42880=EDGE_CURVE ( 'NONE', #13981, #15078, #26523, .T. ) ;
#42946=CIRCLE ( 'NONE', #20305, 23.50000000000000000 ) ;
#43080=EDGE_CURVE ( 'NONE', #7773, #6636, #22333, .T. ) ;
#43150=UNCERTAINTY_MEASURE_WITH_UNIT (LENGTH_MEASURE( 1.000000000000000082E-05 ), #32260, 'distance_accuracy_value', 'NONE');
#43185=VERTEX_POINT ( 'NONE', #9656 ) ;
#43237=EDGE_CURVE ( 'NONE', #28919, #39247, #48278, .T. ) ;
#43287=CIRCLE ( 'NONE', #1421, 7.599999999999996092 ) ;
#43377=ORIENTED_EDGE ( 'NONE', *, *, #15289, .F. ) ;
#43444=EDGE_CURVE ( 'NONE', #15377, #42024, #13200, .T. ) ;
#43480=ORIENTED_EDGE ( 'NONE', *, *, #16566, .F. ) ;
#43489=DIRECTION ( 'NONE',  ( 0.000000000000000000, -1.000000000000000000, 0.000000000000000000 ) ) ;
#43573=DIRECTION ( 'NONE',  ( 0.000000000000000000, 0.000000000000000000, -1.000000000000000000 ) ) ;
#43610=DIRECTION ( 'NONE',  ( 0.000000000000000000, -1.000000000000000000, 0.000000000000000000 ) ) ;
#43619=CARTESIAN_POINT ( 'NONE',  ( 30.68460988201149320, -15.41618894467931611, -103.0993275156849762 ) ) ;
#43642=AXIS2_PLACEMENT_3D ( 'NONE', #48995, #17018, #24322 ) ;
#43699=CARTESIAN_POINT ( 'NONE',  ( 68.13393739769618662, -5.818188944679350882, -65.65000000000000568 ) ) ;
#43702=AXIS2_PLACEMENT_3D ( 'NONE', #14866, #35294, #30830 ) ;
#43743=DIRECTION ( 'NONE',  ( 0.8090169943749515591, 0.000000000000000000, 0.5877852522924675860 ) ) ;
#43821=ORIENTED_EDGE ( 'NONE', *, *, #51310, .T. ) ;
#43868=AXIS2_PLACEMENT_3D ( 'NONE', #23704, #3569, #4323 ) ;
#43885=MANIFOLD_SOLID_BREP ( 'Stock-MAS-691-1', #26822 ) ;
#43887=DIRECTION ( 'NONE',  ( 1.000000000000000000, 0.000000000000000000, 0.000000000000000000 ) ) ;
#43892=ORIENTED_EDGE ( 'NONE', *, *, #984, .T. ) ;
#43895=PLANE ( 'NONE',  #7694 ) ;
#43923=FACE_BOUND ( 'NONE', #31869, .T. ) ;
#43941=VERTEX_POINT ( 'NONE', #4207 ) ;
#44031=ORIENTED_EDGE ( 'NONE', *, *, #12481, .F. ) ;
#44035=CIRCLE ( 'NONE', #22162, 16.00000000000000000 ) ;
#44044=FILL_AREA_STYLE ('',( #12863 ) ) ;
#44125=CARTESIAN_POINT ( 'NONE',  ( 104.6856170952499809, -2.032350560839140119, -65.65000000000000568 ) ) ;
#44176=CARTESIAN_POINT ( 'NONE',  ( 79.93393739769618378, -31.81618894467930403, -65.65000000000000568 ) ) ;
#44191=EDGE_CURVE ( 'NONE', #40265, #50827, #37499, .T. ) ;
#44206=CARTESIAN_POINT ( 'NONE',  ( 68.13393739769618662, -29.66618894467940137, -65.65000000000000568 ) ) ;
#44268=EDGE_LOOP ( 'NONE', ( #7924, #33102 ) ) ;
#44287=EDGE_CURVE ( 'NONE', #37740, #47321, #1506, .T. ) ;
#44294=AXIS2_PLACEMENT_3D ( 'NONE', #42584, #51476, #47548 ) ;
#44443=DIRECTION ( 'NONE',  ( -1.000000000000000000, 0.000000000000000000, 0.000000000000000000 ) ) ;
#44453=EDGE_LOOP ( 'NONE', ( #22368, #35922, #18675, #18493, #14541 ) ) ;
#44505=DIRECTION ( 'NONE',  ( 0.000000000000000000, 1.000000000000000000, 0.000000000000000000 ) ) ;
#44515=ORIENTED_EDGE ( 'NONE', *, *, #1215, .F. ) ;
#44651=VERTEX_POINT ( 'NONE', #30917 ) ;
#44670=VECTOR ( 'NONE', #32903, 1000.000000000000000 ) ;
#44674=EDGE_CURVE ( 'NONE', #39247, #28919, #51709, .T. ) ;
#44682=AXIS2_PLACEMENT_3D ( 'NONE', #43699, #23753, #16621 ) ;
#44737=CARTESIAN_POINT ( 'NONE',  ( 68.13393739769618662, -28.66618894467939782, -65.65000000000000568 ) ) ;
#44818=CARTESIAN_POINT ( 'NONE',  ( 68.13393739769618662, -1.166188944679350081, -65.65000000000000568 ) ) ;
#44855=ORIENTED_EDGE ( 'NONE', *, *, #5517, .T. ) ;
#44878=FACE_OUTER_BOUND ( 'NONE', #28976, .T. ) ;
#44911=EDGE_CURVE ( 'NONE', #13981, #51663, #9882, .T. ) ;
#44981=COLOUR_RGB ( '', 0.40784314, 0.44705882, 0.49803922) ;
#45012=EDGE_CURVE ( 'NONE', #50827, #29283, #50072, .T. ) ;
#45054=ORIENTED_EDGE ( 'NONE', *, *, #26191, .F. ) ;
#45075=DIRECTION ( 'NONE',  ( 8.402539340422011355E-12, -1.000000000000000000, -1.365304166073849981E-11 ) ) ;
#45222=AXIS2_PLACEMENT_3D ( 'NONE', #13302, #32656, #28745 ) ;
#45271=FACE_BOUND ( 'NONE', #36274, .T. ) ;
#45281=DIRECTION ( 'NONE',  ( 0.000000000000000000, -1.000000000000000000, 0.000000000000000000 ) ) ;
#45287=CARTESIAN_POINT ( 'NONE',  ( 68.13393739769618662, -29.66618894467940137, -40.64999999999999858 ) ) ;
#45506=EDGE_LOOP ( 'NONE', ( #35702, #9205, #49843, #5486 ) ) ;
#45518=CARTESIAN_POINT ( 'NONE',  ( 68.13393739769618662, -30.31618894467939995, -49.64999999999999858 ) ) ;
#45531=CARTESIAN_POINT ( 'NONE',  ( 68.13393739844677555, -29.16618894467940137, -89.15000000000000568 ) ) ;
#45535=CARTESIAN_POINT ( 'NONE',  ( 61.98540824044663111, -31.81618894467930403, -70.11716791742267674 ) ) ;
#45587=DIRECTION ( 'NONE',  ( -1.000000000000000000, -3.191443934968489902E-12, -8.980656580310985401E-23 ) ) ;
#45593=CARTESIAN_POINT ( 'NONE',  ( 68.13393739769598767, -2.032350560840590070, -29.09832030244560741 ) ) ;
#45596=FACE_OUTER_BOUND ( 'NONE', #40813, .T. ) ;
#45632=FACE_OUTER_BOUND ( 'NONE', #9345, .T. ) ;
#45741=DIRECTION ( 'NONE',  ( -1.000000000000000000, 0.000000000000000000, 0.000000000000000000 ) ) ;
#45812=FACE_OUTER_BOUND ( 'NONE', #44453, .T. ) ;
#45851=DIRECTION ( 'NONE',  ( 3.191891195582396227E-12, -1.000000000000000000, 0.000000000000000000 ) ) ;
#45857=CARTESIAN_POINT ( 'NONE',  ( 105.5832649133809724, -15.41618894467840484, -65.65000000000004832 ) ) ;
#45871=ORIENTED_EDGE ( 'NONE', *, *, #35076, .T. ) ;
#45917=CARTESIAN_POINT ( 'NONE',  ( 68.13393739769618662, -28.80002732851770020, -65.65000000000000568 ) ) ;
#46011=CARTESIAN_POINT ( 'NONE',  ( 68.13393739769618662, -30.31618894467939995, -65.65000000000000568 ) ) ;
#46115=AXIS2_PLACEMENT_3D ( 'NONE', #34894, #6880, #2412 ) ;
#46130=FACE_OUTER_BOUND ( 'NONE', #35775, .T. ) ;
#46144=EDGE_CURVE ( 'NONE', #29490, #19827, #24140, .T. ) ;
#46152=CIRCLE ( 'NONE', #26890, 1.000000000000000888 ) ;
#46231=ORIENTED_EDGE ( 'NONE', *, *, #12554, .T. ) ;
#46255=DIRECTION ( 'NONE',  ( -1.000000000000000000, 0.000000000000000000, 0.000000000000000000 ) ) ;
#46305=DIRECTION ( 'NONE',  ( 0.000000000000000000, -1.000000000000000000, 0.000000000000000000 ) ) ;
#46385=CARTESIAN_POINT ( 'NONE',  ( 104.6856170952499951, -2.032350560839819131, -29.09832030244561807 ) ) ;
#46386=DIRECTION ( 'NONE',  ( -1.000000000000000000, 0.000000000000000000, 0.000000000000000000 ) ) ;
#46405=EDGE_CURVE ( 'NONE', #29490, #48087, #10838, .T. ) ;
#46418=ORIENTED_EDGE ( 'NONE', *, *, #43237, .T. ) ;
#46491=CARTESIAN_POINT ( 'NONE',  ( 68.13393739769618662, -1.166188944679350081, -65.65000000000000568 ) ) ;
#46507=AXIS2_PLACEMENT_3D ( 'NONE', #8136, #45587, #45851 ) ;
#46528=CARTESIAN_POINT ( 'NONE',  ( 68.13393739769618662, -30.31618894467939995, -65.65000000000000568 ) ) ;
#46688=PRODUCT ( 'Caster Wheel Tread', 'Caster Wheel Tread', '', ( #27779 ) ) ;
#47047=CARTESIAN_POINT ( 'NONE',  ( 104.6856170952509757, -28.80002732851810521, -65.65000000000000568 ) ) ;
#47082=CARTESIAN_POINT ( 'NONE',  ( 68.13393739769618662, -30.31618894467939995, -65.65000000000000568 ) ) ;
#47151=CARTESIAN_POINT ( 'NONE',  ( 68.13393739769618662, -0.5161889446793590519, -51.14999999999999858 ) ) ;
#47321=VERTEX_POINT ( 'NONE', #23381 ) ;
#47331=ORIENTED_EDGE ( 'NONE', *, *, #24812, .F. ) ;
#47370=CARTESIAN_POINT ( 'NONE',  ( 68.13393739769618662, 0.9838110553206419473, -80.15000000000000568 ) ) ;
#47408=DIRECTION ( 'NONE',  ( 0.000000000000000000, 0.000000000000000000, -1.000000000000000000 ) ) ;
#47461=DIRECTION ( 'NONE',  ( 1.000000000000000000, 0.000000000000000000, 0.000000000000000000 ) ) ;
#47467=AXIS2_PLACEMENT_3D ( 'NONE', #15651, #15138, #35301 ) ;
#47548=DIRECTION ( 'NONE',  ( 1.000000000000000000, 0.000000000000000000, 0.000000000000000000 ) ) ;
#47627=AXIS2_PLACEMENT_3D ( 'NONE', #19660, #50869, #15225 ) ;
#47643=CIRCLE ( 'NONE', #5775, 1.000000000000000888 ) ;
#47671=VECTOR ( 'NONE', #50234, 1000.000000000000000 ) ;
#47672=ORIENTED_EDGE ( 'NONE', *, *, #28323, .F. ) ;
#47701=CARTESIAN_POINT ( 'NONE',  ( 84.13393739769618662, -0.5161889446793590519, -65.65000000000000568 ) ) ;
#47768=ORIENTED_EDGE ( 'NONE', *, *, #44911, .F. ) ;
#47798=FACE_OUTER_BOUND ( 'NONE', #12753, .T. ) ;
#47857=AXIS2_PLACEMENT_3D ( 'NONE', #44206, #186, #32381 ) ;
#47986=( NAMED_UNIT ( * ) SI_UNIT ( $, .STERADIAN. ) SOLID_ANGLE_UNIT ( ) );
#48064=CARTESIAN_POINT ( 'NONE',  ( 68.13393739769598767, -2.032350560840590070, -29.09832030244560741 ) ) ;
#48071=CARTESIAN_POINT ( 'NONE',  ( 68.13393739769618662, -0.5161889446793590519, -65.65000000000000568 ) ) ;
#48073=ORIENTED_EDGE ( 'NONE', *, *, #26191, .T. ) ;
#48085=DIRECTION ( 'NONE',  ( 1.000000000000000000, 0.000000000000000000, 0.000000000000000000 ) ) ;
#48087=VERTEX_POINT ( 'NONE', #23475 ) ;
#48127=ORIENTED_EDGE ( 'NONE', *, *, #43237, .F. ) ;
#48143=CARTESIAN_POINT ( 'NONE',  ( 52.13393739769618662, -30.31618894467939995, -65.65000000000000568 ) ) ;
#48159=AXIS2_PLACEMENT_3D ( 'NONE', #9383, #29774, #25327 ) ;
#48161=VERTEX_POINT ( 'NONE', #31341 ) ;
#48203=EDGE_CURVE ( 'NONE', #24462, #37740, #8032, .T. ) ;
#48218=DIRECTION ( 'NONE',  ( 0.000000000000000000, 0.000000000000000000, -1.000000000000000000 ) ) ;
#48236=CIRCLE ( 'NONE', #13902, 34.55616290057869833 ) ;
#48238=SURFACE_SIDE_STYLE ('',( #8927 ) ) ;
#48278=CIRCLE ( 'NONE', #47467, 36.55167969755429880 ) ;
#48376=DIRECTION ( 'NONE',  ( 0.000000000000000000, 1.000000000000000000, 0.000000000000000000 ) ) ;
#48413=CARTESIAN_POINT ( 'NONE',  ( 68.13393739771727553, -29.66618894467940137, -81.65000000000000568 ) ) ;
#48421=ORIENTED_EDGE ( 'NONE', *, *, #14892, .F. ) ;
#48441=DIRECTION ( 'NONE',  ( 0.000000000000000000, 0.000000000000000000, -1.000000000000000000 ) ) ;
#48561=EDGE_CURVE ( 'NONE', #51663, #44651, #35983, .T. ) ;
#48693=CARTESIAN_POINT ( 'NONE',  ( 68.13393739769618662, -0.5161889446793590519, -65.65000000000000568 ) ) ;
#48712=DIRECTION ( 'NONE',  ( 0.000000000000000000, -1.000000000000000000, 0.000000000000000000 ) ) ;
#48747=DIRECTION ( 'NONE',  ( 1.000000000000000000, 0.000000000000000000, 0.000000000000000000 ) ) ;
#48758=SURFACE_STYLE_USAGE ( .BOTH. , #48238 ) ;
#48959=FACE_OUTER_BOUND ( 'NONE', #34197, .T. ) ;
#48994=DIRECTION ( 'NONE',  ( 0.000000000000000000, 1.000000000000000000, 0.000000000000000000 ) ) ;
#48995=CARTESIAN_POINT ( 'NONE',  ( 68.13393739769618662, 0.9838110553206419473, -65.65000000000000568 ) ) ;
#49017=CARTESIAN_POINT ( 'NONE',  ( 68.13393739769618662, -0.1661889446793599900, -31.09383709942130380 ) ) ;
#49092=CARTESIAN_POINT ( 'NONE',  ( 68.13393739823159478, -1.166188945610419969, -65.65000000186969942 ) ) ;
#49407=VECTOR ( 'NONE', #17602, 1000.000000000000000 ) ;
#49413=CARTESIAN_POINT ( 'NONE',  ( 68.13393739769618662, -29.16618894467940137, -65.65000000000000568 ) ) ;
#49416=DIRECTION ( 'NONE',  ( 0.5720614028176879140, 0.7071067811865481278, -0.4156269377774475249 ) ) ;
#49448=ORIENTED_EDGE ( 'NONE', *, *, #32309, .T. ) ;
#49473=PRODUCT_DEFINITION_FORMATION_WITH_SPECIFIED_SOURCE ( 'ANY', '', #46688, .NOT_KNOWN. ) ;
#49504=DIRECTION ( 'NONE',  ( 0.000000000000000000, -1.000000000000000000, 0.000000000000000000 ) ) ;
#49507=DIRECTION ( 'NONE',  ( 1.000000000000000000, 0.000000000000000000, 0.000000000000000000 ) ) ;
#49512=VECTOR ( 'NONE', #4154, 1000.000000000000000 ) ;
#49513=ORIENTED_EDGE ( 'NONE', *, *, #44287, .F. ) ;
#49536=DIRECTION ( 'NONE',  ( 0.000000000000000000, 1.000000000000000000, 0.000000000000000000 ) ) ;
#49550=SHAPE_REPRESENTATION ( 'Caster Wheel Tread', ( #20940 ), #20155 ) ;
#49594=CIRCLE ( 'NONE', #21082, 16.00000000000000000 ) ;
#49599=DIRECTION ( 'NONE',  ( 0.000000000000000000, -1.000000000000000000, 0.000000000000000000 ) ) ;
#49611=CARTESIAN_POINT ( 'NONE',  ( 68.13393739769618662, -0.5161889446793590519, -65.65000000000000568 ) ) ;
#49633=ADVANCED_FACE ( 'NONE', ( #46130 ), #36057, .T. ) ;
#49651=AXIS2_PLACEMENT_3D ( 'NONE', #20202, #32754, #16281 ) ;
#49726=FACE_OUTER_BOUND ( 'NONE', #40251, .T. ) ;
#49782=AXIS2_PLACEMENT_3D ( 'NONE', #14700, #7111, #47461 ) ;
#49786=CARTESIAN_POINT ( 'NONE',  ( 68.13393739769625768, -15.41618894467850076, -103.0993275156848910 ) ) ;
#49797=ORIENTED_EDGE ( 'NONE', *, *, #12481, .T. ) ;
#49823=EDGE_CURVE ( 'NONE', #13981, #1527, #22549, .T. ) ;
#49830=DIRECTION ( 'NONE',  ( 0.8090169943749515591, 0.000000000000000000, -0.5877852522924675860 ) ) ;
#49843=ORIENTED_EDGE ( 'NONE', *, *, #45012, .F. ) ;
#49885=AXIS2_PLACEMENT_3D ( 'NONE', #1899, #34364, #26762 ) ;
#49887=ORIENTED_EDGE ( 'NONE', *, *, #4071, .T. ) ;
#49939=DIRECTION ( 'NONE',  ( 0.000000000000000000, -1.000000000000000000, 0.000000000000000000 ) ) ;
#49942=DIRECTION ( 'NONE',  ( 2.806155971274087206E-29, 5.103645611290830066E-11, -1.000000000000000000 ) ) ;
#49955=AXIS2_PLACEMENT_3D ( 'NONE', #49611, #8992, #13700 ) ;
#50003=EDGE_LOOP ( 'NONE', ( #25848, #25549, #8446, #41311, #37161 ) ) ;
#50040=CARTESIAN_POINT ( 'NONE',  ( 68.13393739769658453, -28.80002732851820468, -102.2016796975550079 ) ) ;
#50072=CIRCLE ( 'NONE', #28303, 24.00000000000000000 ) ;
#50223=CIRCLE ( 'NONE', #25907, 2.000000000000001776 ) ;
#50234=DIRECTION ( 'NONE',  ( 0.000000000000000000, -1.000000000000000000, 0.000000000000000000 ) ) ;
#50254=FACE_OUTER_BOUND ( 'NONE', #11920, .T. ) ;
#50283=ADVANCED_FACE ( 'NONE', ( #24170 ), #17400, .F. ) ;
#50289=CARTESIAN_POINT ( 'NONE',  ( 68.13393739769618662, -30.31618894467939995, -65.65000000000000568 ) ) ;
#50307=CARTESIAN_POINT ( 'NONE',  ( 68.13393739769625768, -15.41618894467990764, -28.20067248431510976 ) ) ;
#50368=AXIS2_PLACEMENT_3D ( 'NONE', #37613, #13780, #9844 ) ;
#50407=ORIENTED_EDGE ( 'NONE', *, *, #44911, .T. ) ;
#50446=DIRECTION ( 'NONE',  ( 0.000000000000000000, 1.000000000000000000, 0.000000000000000000 ) ) ;
#50470=EDGE_CURVE ( 'NONE', #17717, #31931, #42630, .T. ) ;
#50476=AXIS2_PLACEMENT_3D ( 'NONE', #2683, #27034, #30951 ) ;
#50506=AXIS2_PLACEMENT_3D ( 'NONE', #30311, #6750, #25849 ) ;
#50520=CARTESIAN_POINT ( 'NONE',  ( 63.19893373200899589, -0.5161889446793590519, -62.06450996101597184 ) ) ;
#50527=ORIENTED_EDGE ( 'NONE', *, *, #29192, .T. ) ;
#50581=CARTESIAN_POINT ( 'NONE',  ( 68.13393739769618662, -30.66618894467940137, -90.65000000000000568 ) ) ;
#50583=TOROIDAL_SURFACE ( 'NONE', #8716, 16.49999999812870044, 0.4999999999096970127 ) ;
#50599=ORIENTED_EDGE ( 'NONE', *, *, #6924, .F. ) ;
#50603=ORIENTED_EDGE ( 'NONE', *, *, #389, .T. ) ;
#50636=DIRECTION ( 'NONE',  ( 0.000000000000000000, -1.000000000000000000, 0.000000000000000000 ) ) ;
#50650=DIRECTION ( 'NONE',  ( 0.000000000000000000, 1.000000000000000000, 0.000000000000000000 ) ) ;
#50678=AXIS2_PLACEMENT_3D ( 'NONE', #4453, #40101, #770 ) ;
#50728=EDGE_LOOP ( 'NONE', ( #50527, #31920, #31732, #38267 ) ) ;
#50790=AXIS2_PLACEMENT_3D ( 'NONE', #24927, #36476, #24408 ) ;
#50827=VERTEX_POINT ( 'NONE', #10319 ) ;
#50860=PRODUCT_DEFINITION_SHAPE ( 'NONE', 'NONE',  #31487 ) ;
#50865=ADVANCED_FACE ( 'NONE', ( #6907 ), #20078, .T. ) ;
#50869=DIRECTION ( 'NONE',  ( -0.000000000000000000, 1.000000000000000000, 0.000000000000000000 ) ) ;
#50936=CIRCLE ( 'NONE', #7433, 6.099999999999994316 ) ;
#50957=CARTESIAN_POINT ( 'NONE',  ( 31.58225770014188427, -28.80002732851970393, -65.65000000000000568 ) ) ;
#51169=CYLINDRICAL_SURFACE ( 'NONE', #23681, 6.099999999999994316 ) ;
#51302=AXIS2_PLACEMENT_3D ( 'NONE', #47082, #6723, #30797 ) ;
#51305=EDGE_CURVE ( 'NONE', #15377, #24229, #29280, .T. ) ;
#51310=EDGE_CURVE ( 'NONE', #42024, #48161, #15116, .T. ) ;
#51321=VECTOR ( 'NONE', #41527, 1000.000000000000000 ) ;
#51476=DIRECTION ( 'NONE',  ( 0.000000000000000000, -1.000000000000000000, 0.000000000000000000 ) ) ;
#51480=CARTESIAN_POINT ( 'NONE',  ( 31.58225770014180256, -2.032350560840031406, -102.2016796975540274 ) ) ;
#51492=EDGE_LOOP ( 'NONE', ( #12707, #20012, #8153, #18212 ) ) ;
#51540=EDGE_LOOP ( 'NONE', ( #99, #8259 ) ) ;
#51557=CIRCLE ( 'NONE', #49885, 24.00000000000000000 ) ;
#51663=VERTEX_POINT ( 'NONE', #14253 ) ;
#51709=CIRCLE ( 'NONE', #34106, 36.55167969755429880 ) ;
#51780=AXIS2_PLACEMENT_3D ( 'NONE', #42736, #27758, #27236 ) ;
ENDSEC;
END-ISO-10303-21;
